ISO-10303-21;
HEADER;
/* Generated by software containing ST-Developer
 * from STEP Tools, Inc. (www.steptools.com) 
 */

FILE_DESCRIPTION(
/* description */ ('PAT-026'),
/* implementation_level */ '2;1');

FILE_NAME(
/* name */ 'Hub A.step',
/* time_stamp */ '2026-10-28T22:25:58-07:00',
/* author */ (''),
/* organization */ (''),
/* preprocessor_version */ 'ST-DEVELOPER v20.2',
/* originating_system */ 'Autodesk Translation Framework v15.17.0.0',
/* authorisation */ '');

FILE_SCHEMA (('AUTOMOTIVE_DESIGN { 1 0 10303 214 3 1 1 }'));
ENDSEC;

DATA;
#10=MECHANICAL_DESIGN_GEOMETRIC_PRESENTATION_REPRESENTATION('',(#148),#12343);
#97=B_SPLINE_CURVE_WITH_KNOTS('',3,(#10475,#10476,#10477,#10478,#10479,
#10480,#10481,#10482,#10483,#10484,#10485,#10486,#10487,#10488,#10489,#10490,
#10491,#10492),.UNSPECIFIED.,.F.,.F.,(4,2,2,2,2,2,2,2,4),(0.,0.0798638474423531,
0.159727694884706,0.239545993340072,0.319364291795438,0.399182590250804,
0.47900088870617,0.558864736148523,0.638728583590876),.UNSPECIFIED.);
#98=B_SPLINE_CURVE_WITH_KNOTS('',3,(#10493,#10494,#10495,#10496,#10497,
#10498,#10499,#10500,#10501,#10502,#10503,#10504,#10505,#10506,#10507,#10508,
#10509,#10510),.UNSPECIFIED.,.F.,.F.,(4,2,2,2,2,2,2,2,4),(0.638728583590876,
0.718592431033229,0.798456278475582,0.878274576930948,0.958092875386314,
1.03791117384168,1.11772947229705,1.1975933197394,1.27745716718175),
 .UNSPECIFIED.);
#99=B_SPLINE_CURVE_WITH_KNOTS('',3,(#10513,#10514,#10515,#10516,#10517,
#10518,#10519,#10520,#10521,#10522,#10523,#10524,#10525,#10526,#10527,#10528,
#10529,#10530,#10531,#10532,#10533,#10534,#10535,#10536,#10537,#10538,#10539,
#10540,#10541,#10542,#10543,#10544,#10545,#10546),.UNSPECIFIED.,.T.,.F.,
(4,2,2,2,2,2,2,2,2,2,2,2,2,2,2,2,4),(0.,0.079239302416133,0.158478604832266,
0.237716399152057,0.316954193471848,0.39619198779164,0.475429782111431,
0.554669084527564,0.633908386943697,0.71314768935983,0.792386991775963,
0.871624786095754,0.950862580415545,1.03010037473534,1.10933816905513,1.18857747147126,
1.26781677388739),.UNSPECIFIED.);
#126=SHAPE_REPRESENTATION_RELATIONSHIP('SRR','None',#12404,#137);
#137=ADVANCED_BREP_SHAPE_REPRESENTATION('',(#157),#12339);
#148=STYLED_ITEM('',(#12526),#157);
#157=MANIFOLD_SOLID_BREP('Body1',#7356);
#185=FACE_BOUND('',#1061,.T.);
#186=FACE_BOUND('',#1090,.T.);
#187=FACE_BOUND('',#1146,.T.);
#188=FACE_BOUND('',#1148,.T.);
#244=PLANE('',#7622);
#245=PLANE('',#7623);
#246=PLANE('',#7624);
#247=PLANE('',#7625);
#248=PLANE('',#7626);
#249=PLANE('',#7627);
#250=PLANE('',#7628);
#251=PLANE('',#7629);
#252=PLANE('',#7630);
#253=PLANE('',#7631);
#254=PLANE('',#7632);
#255=PLANE('',#7633);
#256=PLANE('',#7634);
#257=PLANE('',#7635);
#258=PLANE('',#7636);
#259=PLANE('',#7637);
#260=PLANE('',#7638);
#261=PLANE('',#7639);
#262=PLANE('',#7640);
#263=PLANE('',#7641);
#264=PLANE('',#7643);
#265=PLANE('',#7645);
#266=PLANE('',#7647);
#267=PLANE('',#7649);
#268=PLANE('',#7651);
#269=PLANE('',#7653);
#270=PLANE('',#7655);
#271=PLANE('',#7657);
#272=PLANE('',#7662);
#273=PLANE('',#7663);
#274=PLANE('',#7664);
#275=PLANE('',#7665);
#276=PLANE('',#7666);
#277=PLANE('',#7667);
#278=PLANE('',#7668);
#279=PLANE('',#7669);
#280=PLANE('',#7670);
#281=PLANE('',#7671);
#282=PLANE('',#7672);
#283=PLANE('',#7673);
#284=PLANE('',#7674);
#285=PLANE('',#7675);
#286=PLANE('',#7676);
#287=PLANE('',#7677);
#288=PLANE('',#7678);
#289=PLANE('',#7679);
#290=PLANE('',#7680);
#291=PLANE('',#7681);
#292=PLANE('',#7683);
#293=PLANE('',#7685);
#294=PLANE('',#7687);
#295=PLANE('',#7689);
#296=PLANE('',#7691);
#297=PLANE('',#7693);
#298=PLANE('',#7695);
#299=PLANE('',#7697);
#300=PLANE('',#7698);
#301=PLANE('',#7699);
#302=PLANE('',#7700);
#303=PLANE('',#7701);
#304=PLANE('',#7702);
#305=PLANE('',#7703);
#306=PLANE('',#7704);
#307=PLANE('',#7705);
#308=PLANE('',#7706);
#309=PLANE('',#7707);
#310=PLANE('',#7708);
#311=PLANE('',#7709);
#312=PLANE('',#7710);
#313=PLANE('',#7711);
#314=PLANE('',#7712);
#315=PLANE('',#7713);
#316=PLANE('',#7714);
#317=PLANE('',#7715);
#318=PLANE('',#7716);
#319=PLANE('',#7718);
#320=PLANE('',#7720);
#321=PLANE('',#7722);
#322=PLANE('',#7724);
#323=PLANE('',#7726);
#324=PLANE('',#7728);
#325=PLANE('',#7730);
#326=PLANE('',#7734);
#632=FACE_OUTER_BOUND('',#1059,.T.);
#633=FACE_OUTER_BOUND('',#1060,.T.);
#634=FACE_OUTER_BOUND('',#1062,.T.);
#635=FACE_OUTER_BOUND('',#1063,.T.);
#636=FACE_OUTER_BOUND('',#1064,.T.);
#637=FACE_OUTER_BOUND('',#1065,.T.);
#638=FACE_OUTER_BOUND('',#1066,.T.);
#639=FACE_OUTER_BOUND('',#1067,.T.);
#640=FACE_OUTER_BOUND('',#1068,.T.);
#641=FACE_OUTER_BOUND('',#1069,.T.);
#642=FACE_OUTER_BOUND('',#1070,.T.);
#643=FACE_OUTER_BOUND('',#1071,.T.);
#644=FACE_OUTER_BOUND('',#1072,.T.);
#645=FACE_OUTER_BOUND('',#1073,.T.);
#646=FACE_OUTER_BOUND('',#1074,.T.);
#647=FACE_OUTER_BOUND('',#1075,.T.);
#648=FACE_OUTER_BOUND('',#1076,.T.);
#649=FACE_OUTER_BOUND('',#1077,.T.);
#650=FACE_OUTER_BOUND('',#1078,.T.);
#651=FACE_OUTER_BOUND('',#1079,.T.);
#652=FACE_OUTER_BOUND('',#1080,.T.);
#653=FACE_OUTER_BOUND('',#1081,.T.);
#654=FACE_OUTER_BOUND('',#1082,.T.);
#655=FACE_OUTER_BOUND('',#1083,.T.);
#656=FACE_OUTER_BOUND('',#1084,.T.);
#657=FACE_OUTER_BOUND('',#1085,.T.);
#658=FACE_OUTER_BOUND('',#1086,.T.);
#659=FACE_OUTER_BOUND('',#1087,.T.);
#660=FACE_OUTER_BOUND('',#1088,.T.);
#661=FACE_OUTER_BOUND('',#1089,.T.);
#662=FACE_OUTER_BOUND('',#1091,.T.);
#663=FACE_OUTER_BOUND('',#1092,.T.);
#664=FACE_OUTER_BOUND('',#1093,.T.);
#665=FACE_OUTER_BOUND('',#1094,.T.);
#666=FACE_OUTER_BOUND('',#1095,.T.);
#667=FACE_OUTER_BOUND('',#1096,.T.);
#668=FACE_OUTER_BOUND('',#1097,.T.);
#669=FACE_OUTER_BOUND('',#1098,.T.);
#670=FACE_OUTER_BOUND('',#1099,.T.);
#671=FACE_OUTER_BOUND('',#1100,.T.);
#672=FACE_OUTER_BOUND('',#1101,.T.);
#673=FACE_OUTER_BOUND('',#1102,.T.);
#674=FACE_OUTER_BOUND('',#1103,.T.);
#675=FACE_OUTER_BOUND('',#1104,.T.);
#676=FACE_OUTER_BOUND('',#1105,.T.);
#677=FACE_OUTER_BOUND('',#1106,.T.);
#678=FACE_OUTER_BOUND('',#1107,.T.);
#679=FACE_OUTER_BOUND('',#1108,.T.);
#680=FACE_OUTER_BOUND('',#1109,.T.);
#681=FACE_OUTER_BOUND('',#1110,.T.);
#682=FACE_OUTER_BOUND('',#1111,.T.);
#683=FACE_OUTER_BOUND('',#1112,.T.);
#684=FACE_OUTER_BOUND('',#1113,.T.);
#685=FACE_OUTER_BOUND('',#1114,.T.);
#686=FACE_OUTER_BOUND('',#1115,.T.);
#687=FACE_OUTER_BOUND('',#1116,.T.);
#688=FACE_OUTER_BOUND('',#1117,.T.);
#689=FACE_OUTER_BOUND('',#1118,.T.);
#690=FACE_OUTER_BOUND('',#1119,.T.);
#691=FACE_OUTER_BOUND('',#1120,.T.);
#692=FACE_OUTER_BOUND('',#1121,.T.);
#693=FACE_OUTER_BOUND('',#1122,.T.);
#694=FACE_OUTER_BOUND('',#1123,.T.);
#695=FACE_OUTER_BOUND('',#1124,.T.);
#696=FACE_OUTER_BOUND('',#1125,.T.);
#697=FACE_OUTER_BOUND('',#1126,.T.);
#698=FACE_OUTER_BOUND('',#1127,.T.);
#699=FACE_OUTER_BOUND('',#1128,.T.);
#700=FACE_OUTER_BOUND('',#1129,.T.);
#701=FACE_OUTER_BOUND('',#1130,.T.);
#702=FACE_OUTER_BOUND('',#1131,.T.);
#703=FACE_OUTER_BOUND('',#1132,.T.);
#704=FACE_OUTER_BOUND('',#1133,.T.);
#705=FACE_OUTER_BOUND('',#1134,.T.);
#706=FACE_OUTER_BOUND('',#1135,.T.);
#707=FACE_OUTER_BOUND('',#1136,.T.);
#708=FACE_OUTER_BOUND('',#1137,.T.);
#709=FACE_OUTER_BOUND('',#1138,.T.);
#710=FACE_OUTER_BOUND('',#1139,.T.);
#711=FACE_OUTER_BOUND('',#1140,.T.);
#712=FACE_OUTER_BOUND('',#1141,.T.);
#713=FACE_OUTER_BOUND('',#1142,.T.);
#714=FACE_OUTER_BOUND('',#1143,.T.);
#715=FACE_OUTER_BOUND('',#1144,.T.);
#716=FACE_OUTER_BOUND('',#1145,.T.);
#717=FACE_OUTER_BOUND('',#1147,.T.);
#1059=EDGE_LOOP('',(#5235,#5236,#5237,#5238,#5239));
#1060=EDGE_LOOP('',(#5240,#5241,#5242,#5243));
#1061=EDGE_LOOP('',(#5244,#5245));
#1062=EDGE_LOOP('',(#5246,#5247,#5248,#5249));
#1063=EDGE_LOOP('',(#5250,#5251,#5252,#5253));
#1064=EDGE_LOOP('',(#5254,#5255,#5256,#5257));
#1065=EDGE_LOOP('',(#5258,#5259,#5260,#5261));
#1066=EDGE_LOOP('',(#5262,#5263,#5264,#5265));
#1067=EDGE_LOOP('',(#5266,#5267,#5268,#5269));
#1068=EDGE_LOOP('',(#5270,#5271,#5272,#5273));
#1069=EDGE_LOOP('',(#5274,#5275,#5276,#5277));
#1070=EDGE_LOOP('',(#5278,#5279,#5280,#5281));
#1071=EDGE_LOOP('',(#5282,#5283,#5284,#5285));
#1072=EDGE_LOOP('',(#5286,#5287,#5288,#5289));
#1073=EDGE_LOOP('',(#5290,#5291,#5292,#5293));
#1074=EDGE_LOOP('',(#5294,#5295,#5296,#5297));
#1075=EDGE_LOOP('',(#5298,#5299,#5300,#5301));
#1076=EDGE_LOOP('',(#5302,#5303,#5304,#5305));
#1077=EDGE_LOOP('',(#5306,#5307,#5308,#5309));
#1078=EDGE_LOOP('',(#5310,#5311,#5312,#5313));
#1079=EDGE_LOOP('',(#5314,#5315,#5316,#5317));
#1080=EDGE_LOOP('',(#5318,#5319,#5320,#5321,#5322,#5323,#5324,#5325,#5326,
#5327,#5328,#5329,#5330,#5331,#5332,#5333,#5334,#5335));
#1081=EDGE_LOOP('',(#5336,#5337));
#1082=EDGE_LOOP('',(#5338,#5339));
#1083=EDGE_LOOP('',(#5340,#5341));
#1084=EDGE_LOOP('',(#5342,#5343));
#1085=EDGE_LOOP('',(#5344,#5345));
#1086=EDGE_LOOP('',(#5346,#5347));
#1087=EDGE_LOOP('',(#5348,#5349));
#1088=EDGE_LOOP('',(#5350,#5351));
#1089=EDGE_LOOP('',(#5352,#5353,#5354,#5355,#5356,#5357,#5358,#5359,#5360,
#5361,#5362,#5363,#5364,#5365,#5366,#5367,#5368,#5369,#5370,#5371,#5372,
#5373,#5374,#5375,#5376,#5377,#5378,#5379,#5380,#5381,#5382,#5383,#5384,
#5385));
#1090=EDGE_LOOP('',(#5386));
#1091=EDGE_LOOP('',(#5387,#5388,#5389,#5390));
#1092=EDGE_LOOP('',(#5391,#5392,#5393,#5394));
#1093=EDGE_LOOP('',(#5395,#5396,#5397,#5398));
#1094=EDGE_LOOP('',(#5399,#5400,#5401,#5402));
#1095=EDGE_LOOP('',(#5403,#5404,#5405,#5406));
#1096=EDGE_LOOP('',(#5407,#5408,#5409,#5410));
#1097=EDGE_LOOP('',(#5411,#5412,#5413,#5414));
#1098=EDGE_LOOP('',(#5415,#5416,#5417,#5418));
#1099=EDGE_LOOP('',(#5419,#5420,#5421,#5422));
#1100=EDGE_LOOP('',(#5423,#5424,#5425,#5426));
#1101=EDGE_LOOP('',(#5427,#5428,#5429,#5430));
#1102=EDGE_LOOP('',(#5431,#5432,#5433,#5434));
#1103=EDGE_LOOP('',(#5435,#5436,#5437,#5438));
#1104=EDGE_LOOP('',(#5439,#5440,#5441,#5442));
#1105=EDGE_LOOP('',(#5443,#5444,#5445,#5446));
#1106=EDGE_LOOP('',(#5447,#5448,#5449,#5450));
#1107=EDGE_LOOP('',(#5451,#5452,#5453,#5454));
#1108=EDGE_LOOP('',(#5455,#5456,#5457,#5458));
#1109=EDGE_LOOP('',(#5459,#5460,#5461,#5462,#5463,#5464,#5465,#5466,#5467,
#5468,#5469,#5470,#5471,#5472,#5473,#5474,#5475,#5476));
#1110=EDGE_LOOP('',(#5477,#5478));
#1111=EDGE_LOOP('',(#5479,#5480));
#1112=EDGE_LOOP('',(#5481,#5482));
#1113=EDGE_LOOP('',(#5483,#5484));
#1114=EDGE_LOOP('',(#5485,#5486));
#1115=EDGE_LOOP('',(#5487,#5488));
#1116=EDGE_LOOP('',(#5489,#5490));
#1117=EDGE_LOOP('',(#5491,#5492));
#1118=EDGE_LOOP('',(#5493,#5494,#5495,#5496));
#1119=EDGE_LOOP('',(#5497,#5498,#5499,#5500));
#1120=EDGE_LOOP('',(#5501,#5502,#5503,#5504));
#1121=EDGE_LOOP('',(#5505,#5506,#5507,#5508));
#1122=EDGE_LOOP('',(#5509,#5510,#5511,#5512));
#1123=EDGE_LOOP('',(#5513,#5514,#5515,#5516));
#1124=EDGE_LOOP('',(#5517,#5518,#5519,#5520));
#1125=EDGE_LOOP('',(#5521,#5522,#5523,#5524));
#1126=EDGE_LOOP('',(#5525,#5526,#5527,#5528));
#1127=EDGE_LOOP('',(#5529,#5530,#5531,#5532));
#1128=EDGE_LOOP('',(#5533,#5534,#5535,#5536));
#1129=EDGE_LOOP('',(#5537,#5538,#5539,#5540));
#1130=EDGE_LOOP('',(#5541,#5542,#5543,#5544));
#1131=EDGE_LOOP('',(#5545,#5546,#5547,#5548));
#1132=EDGE_LOOP('',(#5549,#5550,#5551,#5552));
#1133=EDGE_LOOP('',(#5553,#5554,#5555,#5556));
#1134=EDGE_LOOP('',(#5557,#5558,#5559,#5560));
#1135=EDGE_LOOP('',(#5561,#5562,#5563,#5564));
#1136=EDGE_LOOP('',(#5565,#5566,#5567,#5568,#5569,#5570,#5571,#5572,#5573,
#5574,#5575,#5576,#5577,#5578,#5579,#5580,#5581,#5582));
#1137=EDGE_LOOP('',(#5583,#5584));
#1138=EDGE_LOOP('',(#5585,#5586));
#1139=EDGE_LOOP('',(#5587,#5588));
#1140=EDGE_LOOP('',(#5589,#5590));
#1141=EDGE_LOOP('',(#5591,#5592));
#1142=EDGE_LOOP('',(#5593,#5594));
#1143=EDGE_LOOP('',(#5595,#5596));
#1144=EDGE_LOOP('',(#5597,#5598));
#1145=EDGE_LOOP('',(#5599,#5600,#5601,#5602,#5603,#5604,#5605,#5606,#5607,
#5608,#5609,#5610,#5611,#5612,#5613,#5614,#5615,#5616,#5617,#5618,#5619,
#5620,#5621,#5622,#5623,#5624,#5625,#5626,#5627,#5628,#5629));
#1146=EDGE_LOOP('',(#5630));
#1147=EDGE_LOOP('',(#5631));
#1148=EDGE_LOOP('',(#5632));
#1511=LINE('',#10512,#2383);
#1512=LINE('',#10551,#2384);
#1513=LINE('',#10556,#2385);
#1514=LINE('',#10558,#2386);
#1515=LINE('',#10560,#2387);
#1516=LINE('',#10561,#2388);
#1517=LINE('',#10564,#2389);
#1518=LINE('',#10566,#2390);
#1519=LINE('',#10567,#2391);
#1520=LINE('',#10570,#2392);
#1521=LINE('',#10572,#2393);
#1522=LINE('',#10573,#2394);
#1523=LINE('',#10576,#2395);
#1524=LINE('',#10578,#2396);
#1525=LINE('',#10579,#2397);
#1526=LINE('',#10582,#2398);
#1527=LINE('',#10584,#2399);
#1528=LINE('',#10585,#2400);
#1529=LINE('',#10588,#2401);
#1530=LINE('',#10590,#2402);
#1531=LINE('',#10591,#2403);
#1532=LINE('',#10594,#2404);
#1533=LINE('',#10596,#2405);
#1534=LINE('',#10597,#2406);
#1535=LINE('',#10600,#2407);
#1536=LINE('',#10602,#2408);
#1537=LINE('',#10603,#2409);
#1538=LINE('',#10606,#2410);
#1539=LINE('',#10608,#2411);
#1540=LINE('',#10609,#2412);
#1541=LINE('',#10612,#2413);
#1542=LINE('',#10614,#2414);
#1543=LINE('',#10615,#2415);
#1544=LINE('',#10618,#2416);
#1545=LINE('',#10620,#2417);
#1546=LINE('',#10621,#2418);
#1547=LINE('',#10624,#2419);
#1548=LINE('',#10626,#2420);
#1549=LINE('',#10627,#2421);
#1550=LINE('',#10630,#2422);
#1551=LINE('',#10632,#2423);
#1552=LINE('',#10633,#2424);
#1553=LINE('',#10636,#2425);
#1554=LINE('',#10638,#2426);
#1555=LINE('',#10639,#2427);
#1556=LINE('',#10642,#2428);
#1557=LINE('',#10644,#2429);
#1558=LINE('',#10645,#2430);
#1559=LINE('',#10648,#2431);
#1560=LINE('',#10650,#2432);
#1561=LINE('',#10651,#2433);
#1562=LINE('',#10654,#2434);
#1563=LINE('',#10656,#2435);
#1564=LINE('',#10657,#2436);
#1565=LINE('',#10659,#2437);
#1566=LINE('',#10660,#2438);
#1567=LINE('',#10682,#2439);
#1568=LINE('',#10684,#2440);
#1569=LINE('',#10686,#2441);
#1570=LINE('',#10688,#2442);
#1571=LINE('',#10690,#2443);
#1572=LINE('',#10692,#2444);
#1573=LINE('',#10694,#2445);
#1574=LINE('',#10696,#2446);
#1575=LINE('',#10698,#2447);
#1576=LINE('',#10700,#2448);
#1577=LINE('',#10704,#2449);
#1578=LINE('',#10706,#2450);
#1579=LINE('',#10708,#2451);
#1580=LINE('',#10710,#2452);
#1581=LINE('',#10712,#2453);
#1582=LINE('',#10714,#2454);
#1583=LINE('',#10716,#2455);
#1584=LINE('',#10718,#2456);
#1585=LINE('',#10720,#2457);
#1586=LINE('',#10722,#2458);
#1587=LINE('',#10729,#2459);
#1588=LINE('',#10730,#2460);
#1589=LINE('',#10732,#2461);
#1590=LINE('',#10733,#2462);
#1591=LINE('',#10736,#2463);
#1592=LINE('',#10738,#2464);
#1593=LINE('',#10739,#2465);
#1594=LINE('',#10742,#2466);
#1595=LINE('',#10744,#2467);
#1596=LINE('',#10745,#2468);
#1597=LINE('',#10748,#2469);
#1598=LINE('',#10750,#2470);
#1599=LINE('',#10751,#2471);
#1600=LINE('',#10754,#2472);
#1601=LINE('',#10756,#2473);
#1602=LINE('',#10757,#2474);
#1603=LINE('',#10760,#2475);
#1604=LINE('',#10762,#2476);
#1605=LINE('',#10763,#2477);
#1606=LINE('',#10766,#2478);
#1607=LINE('',#10768,#2479);
#1608=LINE('',#10769,#2480);
#1609=LINE('',#10772,#2481);
#1610=LINE('',#10773,#2482);
#1611=LINE('',#10774,#2483);
#1612=LINE('',#10777,#2484);
#1613=LINE('',#10778,#2485);
#1614=LINE('',#10781,#2486);
#1615=LINE('',#10782,#2487);
#1616=LINE('',#10785,#2488);
#1617=LINE('',#10786,#2489);
#1618=LINE('',#10789,#2490);
#1619=LINE('',#10790,#2491);
#1620=LINE('',#10793,#2492);
#1621=LINE('',#10794,#2493);
#1622=LINE('',#10797,#2494);
#1623=LINE('',#10798,#2495);
#1624=LINE('',#10801,#2496);
#1625=LINE('',#10802,#2497);
#1626=LINE('',#10805,#2498);
#1627=LINE('',#10806,#2499);
#1628=LINE('',#10809,#2500);
#1629=LINE('',#10810,#2501);
#1630=LINE('',#10812,#2502);
#1631=LINE('',#10833,#2503);
#1632=LINE('',#10834,#2504);
#1633=LINE('',#10836,#2505);
#1634=LINE('',#10837,#2506);
#1635=LINE('',#10840,#2507);
#1636=LINE('',#10842,#2508);
#1637=LINE('',#10843,#2509);
#1638=LINE('',#10846,#2510);
#1639=LINE('',#10848,#2511);
#1640=LINE('',#10849,#2512);
#1641=LINE('',#10852,#2513);
#1642=LINE('',#10854,#2514);
#1643=LINE('',#10855,#2515);
#1644=LINE('',#10858,#2516);
#1645=LINE('',#10860,#2517);
#1646=LINE('',#10861,#2518);
#1647=LINE('',#10864,#2519);
#1648=LINE('',#10866,#2520);
#1649=LINE('',#10867,#2521);
#1650=LINE('',#10870,#2522);
#1651=LINE('',#10872,#2523);
#1652=LINE('',#10873,#2524);
#1653=LINE('',#10876,#2525);
#1654=LINE('',#10877,#2526);
#1655=LINE('',#10878,#2527);
#1656=LINE('',#10881,#2528);
#1657=LINE('',#10882,#2529);
#1658=LINE('',#10885,#2530);
#1659=LINE('',#10886,#2531);
#1660=LINE('',#10889,#2532);
#1661=LINE('',#10890,#2533);
#1662=LINE('',#10893,#2534);
#1663=LINE('',#10894,#2535);
#1664=LINE('',#10897,#2536);
#1665=LINE('',#10898,#2537);
#1666=LINE('',#10901,#2538);
#1667=LINE('',#10902,#2539);
#1668=LINE('',#10905,#2540);
#1669=LINE('',#10906,#2541);
#1670=LINE('',#10909,#2542);
#1671=LINE('',#10910,#2543);
#1672=LINE('',#10913,#2544);
#1673=LINE('',#10914,#2545);
#1674=LINE('',#10916,#2546);
#1675=LINE('',#10937,#2547);
#2383=VECTOR('',#8437,0.21);
#2384=VECTOR('',#8442,0.6);
#2385=VECTOR('',#8447,1.);
#2386=VECTOR('',#8448,1.);
#2387=VECTOR('',#8449,1.);
#2388=VECTOR('',#8450,1.);
#2389=VECTOR('',#8453,1.);
#2390=VECTOR('',#8454,1.);
#2391=VECTOR('',#8455,1.);
#2392=VECTOR('',#8458,1.);
#2393=VECTOR('',#8459,1.);
#2394=VECTOR('',#8460,1.);
#2395=VECTOR('',#8463,1.);
#2396=VECTOR('',#8464,1.);
#2397=VECTOR('',#8465,1.);
#2398=VECTOR('',#8468,1.);
#2399=VECTOR('',#8469,1.);
#2400=VECTOR('',#8470,1.);
#2401=VECTOR('',#8473,1.);
#2402=VECTOR('',#8474,1.);
#2403=VECTOR('',#8475,1.);
#2404=VECTOR('',#8478,1.);
#2405=VECTOR('',#8479,1.);
#2406=VECTOR('',#8480,1.);
#2407=VECTOR('',#8483,1.);
#2408=VECTOR('',#8484,1.);
#2409=VECTOR('',#8485,1.);
#2410=VECTOR('',#8488,1.);
#2411=VECTOR('',#8489,1.);
#2412=VECTOR('',#8490,1.);
#2413=VECTOR('',#8493,1.);
#2414=VECTOR('',#8494,1.);
#2415=VECTOR('',#8495,1.);
#2416=VECTOR('',#8498,1.);
#2417=VECTOR('',#8499,1.);
#2418=VECTOR('',#8500,1.);
#2419=VECTOR('',#8503,1.);
#2420=VECTOR('',#8504,1.);
#2421=VECTOR('',#8505,1.);
#2422=VECTOR('',#8508,1.);
#2423=VECTOR('',#8509,1.);
#2424=VECTOR('',#8510,1.);
#2425=VECTOR('',#8513,1.);
#2426=VECTOR('',#8514,1.);
#2427=VECTOR('',#8515,1.);
#2428=VECTOR('',#8518,1.);
#2429=VECTOR('',#8519,1.);
#2430=VECTOR('',#8520,1.);
#2431=VECTOR('',#8523,1.);
#2432=VECTOR('',#8524,1.);
#2433=VECTOR('',#8525,1.);
#2434=VECTOR('',#8528,1.);
#2435=VECTOR('',#8529,1.);
#2436=VECTOR('',#8530,1.);
#2437=VECTOR('',#8533,1.);
#2438=VECTOR('',#8534,1.);
#2439=VECTOR('',#8573,1.);
#2440=VECTOR('',#8574,1.);
#2441=VECTOR('',#8575,1.);
#2442=VECTOR('',#8576,1.);
#2443=VECTOR('',#8577,1.);
#2444=VECTOR('',#8578,1.);
#2445=VECTOR('',#8579,1.);
#2446=VECTOR('',#8580,1.);
#2447=VECTOR('',#8581,1.);
#2448=VECTOR('',#8582,1.);
#2449=VECTOR('',#8585,1.);
#2450=VECTOR('',#8586,1.);
#2451=VECTOR('',#8587,1.);
#2452=VECTOR('',#8588,1.);
#2453=VECTOR('',#8589,1.);
#2454=VECTOR('',#8590,1.);
#2455=VECTOR('',#8591,1.);
#2456=VECTOR('',#8592,1.);
#2457=VECTOR('',#8593,1.);
#2458=VECTOR('',#8594,1.);
#2459=VECTOR('',#8601,1.);
#2460=VECTOR('',#8602,1.);
#2461=VECTOR('',#8603,1.);
#2462=VECTOR('',#8604,1.);
#2463=VECTOR('',#8607,1.);
#2464=VECTOR('',#8608,1.);
#2465=VECTOR('',#8609,1.);
#2466=VECTOR('',#8612,1.);
#2467=VECTOR('',#8613,1.);
#2468=VECTOR('',#8614,1.);
#2469=VECTOR('',#8617,1.);
#2470=VECTOR('',#8618,1.);
#2471=VECTOR('',#8619,1.);
#2472=VECTOR('',#8622,1.);
#2473=VECTOR('',#8623,1.);
#2474=VECTOR('',#8624,1.);
#2475=VECTOR('',#8627,1.);
#2476=VECTOR('',#8628,1.);
#2477=VECTOR('',#8629,1.);
#2478=VECTOR('',#8632,1.);
#2479=VECTOR('',#8633,1.);
#2480=VECTOR('',#8634,1.);
#2481=VECTOR('',#8637,1.);
#2482=VECTOR('',#8638,1.);
#2483=VECTOR('',#8639,1.);
#2484=VECTOR('',#8642,1.);
#2485=VECTOR('',#8643,1.);
#2486=VECTOR('',#8646,1.);
#2487=VECTOR('',#8647,1.);
#2488=VECTOR('',#8650,1.);
#2489=VECTOR('',#8651,1.);
#2490=VECTOR('',#8654,1.);
#2491=VECTOR('',#8655,1.);
#2492=VECTOR('',#8658,1.);
#2493=VECTOR('',#8659,1.);
#2494=VECTOR('',#8662,1.);
#2495=VECTOR('',#8663,1.);
#2496=VECTOR('',#8666,1.);
#2497=VECTOR('',#8667,1.);
#2498=VECTOR('',#8670,1.);
#2499=VECTOR('',#8671,1.);
#2500=VECTOR('',#8674,1.);
#2501=VECTOR('',#8675,1.);
#2502=VECTOR('',#8678,1.);
#2503=VECTOR('',#8715,1.);
#2504=VECTOR('',#8716,1.);
#2505=VECTOR('',#8717,1.);
#2506=VECTOR('',#8718,1.);
#2507=VECTOR('',#8721,1.);
#2508=VECTOR('',#8722,1.);
#2509=VECTOR('',#8723,1.);
#2510=VECTOR('',#8726,1.);
#2511=VECTOR('',#8727,1.);
#2512=VECTOR('',#8728,1.);
#2513=VECTOR('',#8731,1.);
#2514=VECTOR('',#8732,1.);
#2515=VECTOR('',#8733,1.);
#2516=VECTOR('',#8736,1.);
#2517=VECTOR('',#8737,1.);
#2518=VECTOR('',#8738,1.);
#2519=VECTOR('',#8741,1.);
#2520=VECTOR('',#8742,1.);
#2521=VECTOR('',#8743,1.);
#2522=VECTOR('',#8746,1.);
#2523=VECTOR('',#8747,1.);
#2524=VECTOR('',#8748,1.);
#2525=VECTOR('',#8751,1.);
#2526=VECTOR('',#8752,1.);
#2527=VECTOR('',#8753,1.);
#2528=VECTOR('',#8756,1.);
#2529=VECTOR('',#8757,1.);
#2530=VECTOR('',#8760,1.);
#2531=VECTOR('',#8761,1.);
#2532=VECTOR('',#8764,1.);
#2533=VECTOR('',#8765,1.);
#2534=VECTOR('',#8768,1.);
#2535=VECTOR('',#8769,1.);
#2536=VECTOR('',#8772,1.);
#2537=VECTOR('',#8773,1.);
#2538=VECTOR('',#8776,1.);
#2539=VECTOR('',#8777,1.);
#2540=VECTOR('',#8780,1.);
#2541=VECTOR('',#8781,1.);
#2542=VECTOR('',#8784,1.);
#2543=VECTOR('',#8785,1.);
#2544=VECTOR('',#8788,1.);
#2545=VECTOR('',#8789,1.);
#2546=VECTOR('',#8792,1.);
#2547=VECTOR('',#8831,1.37);
#3183=CIRCLE('',#7620,0.6);
#3184=CIRCLE('',#7621,0.6);
#3185=CIRCLE('',#7642,1.37);
#3186=CIRCLE('',#7644,1.37);
#3187=CIRCLE('',#7646,1.37);
#3188=CIRCLE('',#7648,1.37);
#3189=CIRCLE('',#7650,1.37);
#3190=CIRCLE('',#7652,1.37);
#3191=CIRCLE('',#7654,1.37);
#3192=CIRCLE('',#7656,1.37);
#3193=CIRCLE('',#7658,1.37);
#3194=CIRCLE('',#7659,1.37);
#3195=CIRCLE('',#7660,1.37);
#3196=CIRCLE('',#7661,1.37);
#3197=CIRCLE('',#7682,1.37);
#3198=CIRCLE('',#7684,1.37);
#3199=CIRCLE('',#7686,1.37);
#3200=CIRCLE('',#7688,1.37);
#3201=CIRCLE('',#7690,1.37);
#3202=CIRCLE('',#7692,1.37);
#3203=CIRCLE('',#7694,1.37);
#3204=CIRCLE('',#7696,1.37);
#3205=CIRCLE('',#7717,1.37);
#3206=CIRCLE('',#7719,1.37);
#3207=CIRCLE('',#7721,1.37);
#3208=CIRCLE('',#7723,1.37);
#3209=CIRCLE('',#7725,1.37);
#3210=CIRCLE('',#7727,1.37);
#3211=CIRCLE('',#7729,1.37);
#3212=CIRCLE('',#7731,1.37);
#3213=CIRCLE('',#7733,1.37);
#3370=VERTEX_POINT('',#10473);
#3371=VERTEX_POINT('',#10474);
#3372=VERTEX_POINT('',#10511);
#3373=VERTEX_POINT('',#10548);
#3374=VERTEX_POINT('',#10550);
#3375=VERTEX_POINT('',#10554);
#3376=VERTEX_POINT('',#10555);
#3377=VERTEX_POINT('',#10557);
#3378=VERTEX_POINT('',#10559);
#3379=VERTEX_POINT('',#10563);
#3380=VERTEX_POINT('',#10565);
#3381=VERTEX_POINT('',#10569);
#3382=VERTEX_POINT('',#10571);
#3383=VERTEX_POINT('',#10575);
#3384=VERTEX_POINT('',#10577);
#3385=VERTEX_POINT('',#10581);
#3386=VERTEX_POINT('',#10583);
#3387=VERTEX_POINT('',#10587);
#3388=VERTEX_POINT('',#10589);
#3389=VERTEX_POINT('',#10593);
#3390=VERTEX_POINT('',#10595);
#3391=VERTEX_POINT('',#10599);
#3392=VERTEX_POINT('',#10601);
#3393=VERTEX_POINT('',#10605);
#3394=VERTEX_POINT('',#10607);
#3395=VERTEX_POINT('',#10611);
#3396=VERTEX_POINT('',#10613);
#3397=VERTEX_POINT('',#10617);
#3398=VERTEX_POINT('',#10619);
#3399=VERTEX_POINT('',#10623);
#3400=VERTEX_POINT('',#10625);
#3401=VERTEX_POINT('',#10629);
#3402=VERTEX_POINT('',#10631);
#3403=VERTEX_POINT('',#10635);
#3404=VERTEX_POINT('',#10637);
#3405=VERTEX_POINT('',#10641);
#3406=VERTEX_POINT('',#10643);
#3407=VERTEX_POINT('',#10647);
#3408=VERTEX_POINT('',#10649);
#3409=VERTEX_POINT('',#10653);
#3410=VERTEX_POINT('',#10655);
#3411=VERTEX_POINT('',#10679);
#3412=VERTEX_POINT('',#10681);
#3413=VERTEX_POINT('',#10683);
#3414=VERTEX_POINT('',#10685);
#3415=VERTEX_POINT('',#10687);
#3416=VERTEX_POINT('',#10689);
#3417=VERTEX_POINT('',#10691);
#3418=VERTEX_POINT('',#10693);
#3419=VERTEX_POINT('',#10695);
#3420=VERTEX_POINT('',#10697);
#3421=VERTEX_POINT('',#10699);
#3422=VERTEX_POINT('',#10701);
#3423=VERTEX_POINT('',#10703);
#3424=VERTEX_POINT('',#10705);
#3425=VERTEX_POINT('',#10707);
#3426=VERTEX_POINT('',#10709);
#3427=VERTEX_POINT('',#10711);
#3428=VERTEX_POINT('',#10713);
#3429=VERTEX_POINT('',#10715);
#3430=VERTEX_POINT('',#10717);
#3431=VERTEX_POINT('',#10719);
#3432=VERTEX_POINT('',#10721);
#3433=VERTEX_POINT('',#10723);
#3434=VERTEX_POINT('',#10727);
#3435=VERTEX_POINT('',#10728);
#3436=VERTEX_POINT('',#10731);
#3437=VERTEX_POINT('',#10735);
#3438=VERTEX_POINT('',#10737);
#3439=VERTEX_POINT('',#10741);
#3440=VERTEX_POINT('',#10743);
#3441=VERTEX_POINT('',#10747);
#3442=VERTEX_POINT('',#10749);
#3443=VERTEX_POINT('',#10753);
#3444=VERTEX_POINT('',#10755);
#3445=VERTEX_POINT('',#10759);
#3446=VERTEX_POINT('',#10761);
#3447=VERTEX_POINT('',#10765);
#3448=VERTEX_POINT('',#10767);
#3449=VERTEX_POINT('',#10771);
#3450=VERTEX_POINT('',#10776);
#3451=VERTEX_POINT('',#10780);
#3452=VERTEX_POINT('',#10784);
#3453=VERTEX_POINT('',#10788);
#3454=VERTEX_POINT('',#10792);
#3455=VERTEX_POINT('',#10796);
#3456=VERTEX_POINT('',#10800);
#3457=VERTEX_POINT('',#10804);
#3458=VERTEX_POINT('',#10808);
#3459=VERTEX_POINT('',#10831);
#3460=VERTEX_POINT('',#10832);
#3461=VERTEX_POINT('',#10835);
#3462=VERTEX_POINT('',#10839);
#3463=VERTEX_POINT('',#10841);
#3464=VERTEX_POINT('',#10845);
#3465=VERTEX_POINT('',#10847);
#3466=VERTEX_POINT('',#10851);
#3467=VERTEX_POINT('',#10853);
#3468=VERTEX_POINT('',#10857);
#3469=VERTEX_POINT('',#10859);
#3470=VERTEX_POINT('',#10863);
#3471=VERTEX_POINT('',#10865);
#3472=VERTEX_POINT('',#10869);
#3473=VERTEX_POINT('',#10871);
#3474=VERTEX_POINT('',#10875);
#3475=VERTEX_POINT('',#10880);
#3476=VERTEX_POINT('',#10884);
#3477=VERTEX_POINT('',#10888);
#3478=VERTEX_POINT('',#10892);
#3479=VERTEX_POINT('',#10896);
#3480=VERTEX_POINT('',#10900);
#3481=VERTEX_POINT('',#10904);
#3482=VERTEX_POINT('',#10908);
#3483=VERTEX_POINT('',#10912);
#3484=VERTEX_POINT('',#10935);
#4061=EDGE_CURVE('',#3370,#3371,#97,.T.);
#4062=EDGE_CURVE('',#3371,#3370,#98,.T.);
#4063=EDGE_CURVE('',#3371,#3372,#1511,.T.);
#4064=EDGE_CURVE('',#3372,#3372,#99,.T.);
#4065=EDGE_CURVE('',#3373,#3373,#3183,.T.);
#4066=EDGE_CURVE('',#3373,#3374,#1512,.T.);
#4067=EDGE_CURVE('',#3374,#3374,#3184,.T.);
#4068=EDGE_CURVE('',#3375,#3376,#1513,.T.);
#4069=EDGE_CURVE('',#3375,#3377,#1514,.T.);
#4070=EDGE_CURVE('',#3378,#3377,#1515,.T.);
#4071=EDGE_CURVE('',#3376,#3378,#1516,.T.);
#4072=EDGE_CURVE('',#3376,#3379,#1517,.T.);
#4073=EDGE_CURVE('',#3380,#3378,#1518,.T.);
#4074=EDGE_CURVE('',#3379,#3380,#1519,.T.);
#4075=EDGE_CURVE('',#3379,#3381,#1520,.T.);
#4076=EDGE_CURVE('',#3382,#3380,#1521,.T.);
#4077=EDGE_CURVE('',#3381,#3382,#1522,.T.);
#4078=EDGE_CURVE('',#3381,#3383,#1523,.T.);
#4079=EDGE_CURVE('',#3384,#3382,#1524,.T.);
#4080=EDGE_CURVE('',#3383,#3384,#1525,.T.);
#4081=EDGE_CURVE('',#3383,#3385,#1526,.T.);
#4082=EDGE_CURVE('',#3386,#3384,#1527,.T.);
#4083=EDGE_CURVE('',#3385,#3386,#1528,.T.);
#4084=EDGE_CURVE('',#3385,#3387,#1529,.T.);
#4085=EDGE_CURVE('',#3388,#3386,#1530,.T.);
#4086=EDGE_CURVE('',#3387,#3388,#1531,.T.);
#4087=EDGE_CURVE('',#3387,#3389,#1532,.T.);
#4088=EDGE_CURVE('',#3390,#3388,#1533,.T.);
#4089=EDGE_CURVE('',#3389,#3390,#1534,.T.);
#4090=EDGE_CURVE('',#3389,#3391,#1535,.T.);
#4091=EDGE_CURVE('',#3392,#3390,#1536,.T.);
#4092=EDGE_CURVE('',#3391,#3392,#1537,.T.);
#4093=EDGE_CURVE('',#3391,#3393,#1538,.T.);
#4094=EDGE_CURVE('',#3394,#3392,#1539,.T.);
#4095=EDGE_CURVE('',#3393,#3394,#1540,.T.);
#4096=EDGE_CURVE('',#3393,#3395,#1541,.T.);
#4097=EDGE_CURVE('',#3396,#3394,#1542,.T.);
#4098=EDGE_CURVE('',#3395,#3396,#1543,.T.);
#4099=EDGE_CURVE('',#3395,#3397,#1544,.T.);
#4100=EDGE_CURVE('',#3398,#3396,#1545,.T.);
#4101=EDGE_CURVE('',#3397,#3398,#1546,.T.);
#4102=EDGE_CURVE('',#3397,#3399,#1547,.T.);
#4103=EDGE_CURVE('',#3400,#3398,#1548,.T.);
#4104=EDGE_CURVE('',#3399,#3400,#1549,.T.);
#4105=EDGE_CURVE('',#3399,#3401,#1550,.T.);
#4106=EDGE_CURVE('',#3402,#3400,#1551,.T.);
#4107=EDGE_CURVE('',#3401,#3402,#1552,.T.);
#4108=EDGE_CURVE('',#3401,#3403,#1553,.T.);
#4109=EDGE_CURVE('',#3404,#3402,#1554,.T.);
#4110=EDGE_CURVE('',#3403,#3404,#1555,.T.);
#4111=EDGE_CURVE('',#3403,#3405,#1556,.T.);
#4112=EDGE_CURVE('',#3406,#3404,#1557,.T.);
#4113=EDGE_CURVE('',#3405,#3406,#1558,.T.);
#4114=EDGE_CURVE('',#3405,#3407,#1559,.T.);
#4115=EDGE_CURVE('',#3408,#3406,#1560,.T.);
#4116=EDGE_CURVE('',#3407,#3408,#1561,.T.);
#4117=EDGE_CURVE('',#3407,#3409,#1562,.T.);
#4118=EDGE_CURVE('',#3410,#3408,#1563,.T.);
#4119=EDGE_CURVE('',#3409,#3410,#1564,.T.);
#4120=EDGE_CURVE('',#3409,#3375,#1565,.T.);
#4121=EDGE_CURVE('',#3377,#3410,#1566,.T.);
#4122=EDGE_CURVE('',#3377,#3378,#3185,.T.);
#4123=EDGE_CURVE('',#3378,#3380,#3186,.T.);
#4124=EDGE_CURVE('',#3380,#3382,#3187,.T.);
#4125=EDGE_CURVE('',#3382,#3384,#3188,.T.);
#4126=EDGE_CURVE('',#3384,#3386,#3189,.T.);
#4127=EDGE_CURVE('',#3386,#3388,#3190,.T.);
#4128=EDGE_CURVE('',#3388,#3390,#3191,.T.);
#4129=EDGE_CURVE('',#3390,#3392,#3192,.T.);
#4130=EDGE_CURVE('',#3392,#3411,#3193,.T.);
#4131=EDGE_CURVE('',#3411,#3412,#1567,.T.);
#4132=EDGE_CURVE('',#3412,#3413,#1568,.T.);
#4133=EDGE_CURVE('',#3413,#3414,#1569,.T.);
#4134=EDGE_CURVE('',#3414,#3415,#1570,.T.);
#4135=EDGE_CURVE('',#3415,#3416,#1571,.T.);
#4136=EDGE_CURVE('',#3416,#3417,#1572,.T.);
#4137=EDGE_CURVE('',#3417,#3418,#1573,.T.);
#4138=EDGE_CURVE('',#3418,#3419,#1574,.T.);
#4139=EDGE_CURVE('',#3419,#3420,#1575,.T.);
#4140=EDGE_CURVE('',#3420,#3421,#1576,.T.);
#4141=EDGE_CURVE('',#3421,#3422,#3194,.T.);
#4142=EDGE_CURVE('',#3422,#3423,#1577,.T.);
#4143=EDGE_CURVE('',#3423,#3424,#1578,.T.);
#4144=EDGE_CURVE('',#3424,#3425,#1579,.T.);
#4145=EDGE_CURVE('',#3425,#3426,#1580,.T.);
#4146=EDGE_CURVE('',#3426,#3427,#1581,.T.);
#4147=EDGE_CURVE('',#3427,#3428,#1582,.T.);
#4148=EDGE_CURVE('',#3428,#3429,#1583,.T.);
#4149=EDGE_CURVE('',#3429,#3430,#1584,.T.);
#4150=EDGE_CURVE('',#3430,#3431,#1585,.T.);
#4151=EDGE_CURVE('',#3431,#3432,#1586,.T.);
#4152=EDGE_CURVE('',#3432,#3433,#3195,.T.);
#4153=EDGE_CURVE('',#3433,#3377,#3196,.T.);
#4154=EDGE_CURVE('',#3434,#3435,#1587,.T.);
#4155=EDGE_CURVE('',#3434,#3422,#1588,.T.);
#4156=EDGE_CURVE('',#3436,#3422,#1589,.T.);
#4157=EDGE_CURVE('',#3435,#3436,#1590,.T.);
#4158=EDGE_CURVE('',#3435,#3437,#1591,.T.);
#4159=EDGE_CURVE('',#3438,#3436,#1592,.T.);
#4160=EDGE_CURVE('',#3437,#3438,#1593,.T.);
#4161=EDGE_CURVE('',#3437,#3439,#1594,.T.);
#4162=EDGE_CURVE('',#3440,#3438,#1595,.T.);
#4163=EDGE_CURVE('',#3439,#3440,#1596,.T.);
#4164=EDGE_CURVE('',#3439,#3441,#1597,.T.);
#4165=EDGE_CURVE('',#3442,#3440,#1598,.T.);
#4166=EDGE_CURVE('',#3441,#3442,#1599,.T.);
#4167=EDGE_CURVE('',#3441,#3443,#1600,.T.);
#4168=EDGE_CURVE('',#3444,#3442,#1601,.T.);
#4169=EDGE_CURVE('',#3443,#3444,#1602,.T.);
#4170=EDGE_CURVE('',#3443,#3445,#1603,.T.);
#4171=EDGE_CURVE('',#3446,#3444,#1604,.T.);
#4172=EDGE_CURVE('',#3445,#3446,#1605,.T.);
#4173=EDGE_CURVE('',#3445,#3447,#1606,.T.);
#4174=EDGE_CURVE('',#3448,#3446,#1607,.T.);
#4175=EDGE_CURVE('',#3447,#3448,#1608,.T.);
#4176=EDGE_CURVE('',#3447,#3449,#1609,.T.);
#4177=EDGE_CURVE('',#3432,#3448,#1610,.T.);
#4178=EDGE_CURVE('',#3449,#3432,#1611,.T.);
#4179=EDGE_CURVE('',#3449,#3450,#1612,.T.);
#4180=EDGE_CURVE('',#3450,#3431,#1613,.T.);
#4181=EDGE_CURVE('',#3450,#3451,#1614,.T.);
#4182=EDGE_CURVE('',#3451,#3430,#1615,.T.);
#4183=EDGE_CURVE('',#3451,#3452,#1616,.T.);
#4184=EDGE_CURVE('',#3452,#3429,#1617,.T.);
#4185=EDGE_CURVE('',#3452,#3453,#1618,.T.);
#4186=EDGE_CURVE('',#3453,#3428,#1619,.T.);
#4187=EDGE_CURVE('',#3453,#3454,#1620,.T.);
#4188=EDGE_CURVE('',#3454,#3427,#1621,.T.);
#4189=EDGE_CURVE('',#3454,#3455,#1622,.T.);
#4190=EDGE_CURVE('',#3455,#3426,#1623,.T.);
#4191=EDGE_CURVE('',#3455,#3456,#1624,.T.);
#4192=EDGE_CURVE('',#3456,#3425,#1625,.T.);
#4193=EDGE_CURVE('',#3456,#3457,#1626,.T.);
#4194=EDGE_CURVE('',#3457,#3424,#1627,.T.);
#4195=EDGE_CURVE('',#3457,#3458,#1628,.T.);
#4196=EDGE_CURVE('',#3458,#3423,#1629,.T.);
#4197=EDGE_CURVE('',#3458,#3434,#1630,.T.);
#4198=EDGE_CURVE('',#3422,#3436,#3197,.T.);
#4199=EDGE_CURVE('',#3436,#3438,#3198,.T.);
#4200=EDGE_CURVE('',#3438,#3440,#3199,.T.);
#4201=EDGE_CURVE('',#3440,#3442,#3200,.T.);
#4202=EDGE_CURVE('',#3442,#3444,#3201,.T.);
#4203=EDGE_CURVE('',#3444,#3446,#3202,.T.);
#4204=EDGE_CURVE('',#3446,#3448,#3203,.T.);
#4205=EDGE_CURVE('',#3448,#3432,#3204,.T.);
#4206=EDGE_CURVE('',#3459,#3460,#1631,.T.);
#4207=EDGE_CURVE('',#3459,#3411,#1632,.T.);
#4208=EDGE_CURVE('',#3461,#3411,#1633,.T.);
#4209=EDGE_CURVE('',#3460,#3461,#1634,.T.);
#4210=EDGE_CURVE('',#3460,#3462,#1635,.T.);
#4211=EDGE_CURVE('',#3463,#3461,#1636,.T.);
#4212=EDGE_CURVE('',#3462,#3463,#1637,.T.);
#4213=EDGE_CURVE('',#3462,#3464,#1638,.T.);
#4214=EDGE_CURVE('',#3465,#3463,#1639,.T.);
#4215=EDGE_CURVE('',#3464,#3465,#1640,.T.);
#4216=EDGE_CURVE('',#3464,#3466,#1641,.T.);
#4217=EDGE_CURVE('',#3467,#3465,#1642,.T.);
#4218=EDGE_CURVE('',#3466,#3467,#1643,.T.);
#4219=EDGE_CURVE('',#3466,#3468,#1644,.T.);
#4220=EDGE_CURVE('',#3469,#3467,#1645,.T.);
#4221=EDGE_CURVE('',#3468,#3469,#1646,.T.);
#4222=EDGE_CURVE('',#3468,#3470,#1647,.T.);
#4223=EDGE_CURVE('',#3471,#3469,#1648,.T.);
#4224=EDGE_CURVE('',#3470,#3471,#1649,.T.);
#4225=EDGE_CURVE('',#3470,#3472,#1650,.T.);
#4226=EDGE_CURVE('',#3473,#3471,#1651,.T.);
#4227=EDGE_CURVE('',#3472,#3473,#1652,.T.);
#4228=EDGE_CURVE('',#3472,#3474,#1653,.T.);
#4229=EDGE_CURVE('',#3421,#3473,#1654,.T.);
#4230=EDGE_CURVE('',#3474,#3421,#1655,.T.);
#4231=EDGE_CURVE('',#3474,#3475,#1656,.T.);
#4232=EDGE_CURVE('',#3475,#3420,#1657,.T.);
#4233=EDGE_CURVE('',#3475,#3476,#1658,.T.);
#4234=EDGE_CURVE('',#3476,#3419,#1659,.T.);
#4235=EDGE_CURVE('',#3476,#3477,#1660,.T.);
#4236=EDGE_CURVE('',#3477,#3418,#1661,.T.);
#4237=EDGE_CURVE('',#3477,#3478,#1662,.T.);
#4238=EDGE_CURVE('',#3478,#3417,#1663,.T.);
#4239=EDGE_CURVE('',#3478,#3479,#1664,.T.);
#4240=EDGE_CURVE('',#3479,#3416,#1665,.T.);
#4241=EDGE_CURVE('',#3479,#3480,#1666,.T.);
#4242=EDGE_CURVE('',#3480,#3415,#1667,.T.);
#4243=EDGE_CURVE('',#3480,#3481,#1668,.T.);
#4244=EDGE_CURVE('',#3481,#3414,#1669,.T.);
#4245=EDGE_CURVE('',#3481,#3482,#1670,.T.);
#4246=EDGE_CURVE('',#3482,#3413,#1671,.T.);
#4247=EDGE_CURVE('',#3482,#3483,#1672,.T.);
#4248=EDGE_CURVE('',#3483,#3412,#1673,.T.);
#4249=EDGE_CURVE('',#3483,#3459,#1674,.T.);
#4250=EDGE_CURVE('',#3411,#3461,#3205,.T.);
#4251=EDGE_CURVE('',#3461,#3463,#3206,.T.);
#4252=EDGE_CURVE('',#3463,#3465,#3207,.T.);
#4253=EDGE_CURVE('',#3465,#3467,#3208,.T.);
#4254=EDGE_CURVE('',#3467,#3469,#3209,.T.);
#4255=EDGE_CURVE('',#3469,#3471,#3210,.T.);
#4256=EDGE_CURVE('',#3471,#3473,#3211,.T.);
#4257=EDGE_CURVE('',#3473,#3421,#3212,.T.);
#4258=EDGE_CURVE('',#3484,#3484,#3213,.T.);
#4259=EDGE_CURVE('',#3484,#3433,#1675,.T.);
#5235=ORIENTED_EDGE('',*,*,#4061,.F.);
#5236=ORIENTED_EDGE('',*,*,#4062,.F.);
#5237=ORIENTED_EDGE('',*,*,#4063,.T.);
#5238=ORIENTED_EDGE('',*,*,#4064,.F.);
#5239=ORIENTED_EDGE('',*,*,#4063,.F.);
#5240=ORIENTED_EDGE('',*,*,#4065,.F.);
#5241=ORIENTED_EDGE('',*,*,#4066,.T.);
#5242=ORIENTED_EDGE('',*,*,#4067,.F.);
#5243=ORIENTED_EDGE('',*,*,#4066,.F.);
#5244=ORIENTED_EDGE('',*,*,#4061,.T.);
#5245=ORIENTED_EDGE('',*,*,#4062,.T.);
#5246=ORIENTED_EDGE('',*,*,#4068,.F.);
#5247=ORIENTED_EDGE('',*,*,#4069,.T.);
#5248=ORIENTED_EDGE('',*,*,#4070,.F.);
#5249=ORIENTED_EDGE('',*,*,#4071,.F.);
#5250=ORIENTED_EDGE('',*,*,#4072,.F.);
#5251=ORIENTED_EDGE('',*,*,#4071,.T.);
#5252=ORIENTED_EDGE('',*,*,#4073,.F.);
#5253=ORIENTED_EDGE('',*,*,#4074,.F.);
#5254=ORIENTED_EDGE('',*,*,#4075,.F.);
#5255=ORIENTED_EDGE('',*,*,#4074,.T.);
#5256=ORIENTED_EDGE('',*,*,#4076,.F.);
#5257=ORIENTED_EDGE('',*,*,#4077,.F.);
#5258=ORIENTED_EDGE('',*,*,#4078,.F.);
#5259=ORIENTED_EDGE('',*,*,#4077,.T.);
#5260=ORIENTED_EDGE('',*,*,#4079,.F.);
#5261=ORIENTED_EDGE('',*,*,#4080,.F.);
#5262=ORIENTED_EDGE('',*,*,#4081,.F.);
#5263=ORIENTED_EDGE('',*,*,#4080,.T.);
#5264=ORIENTED_EDGE('',*,*,#4082,.F.);
#5265=ORIENTED_EDGE('',*,*,#4083,.F.);
#5266=ORIENTED_EDGE('',*,*,#4084,.F.);
#5267=ORIENTED_EDGE('',*,*,#4083,.T.);
#5268=ORIENTED_EDGE('',*,*,#4085,.F.);
#5269=ORIENTED_EDGE('',*,*,#4086,.F.);
#5270=ORIENTED_EDGE('',*,*,#4087,.F.);
#5271=ORIENTED_EDGE('',*,*,#4086,.T.);
#5272=ORIENTED_EDGE('',*,*,#4088,.F.);
#5273=ORIENTED_EDGE('',*,*,#4089,.F.);
#5274=ORIENTED_EDGE('',*,*,#4090,.F.);
#5275=ORIENTED_EDGE('',*,*,#4089,.T.);
#5276=ORIENTED_EDGE('',*,*,#4091,.F.);
#5277=ORIENTED_EDGE('',*,*,#4092,.F.);
#5278=ORIENTED_EDGE('',*,*,#4093,.F.);
#5279=ORIENTED_EDGE('',*,*,#4092,.T.);
#5280=ORIENTED_EDGE('',*,*,#4094,.F.);
#5281=ORIENTED_EDGE('',*,*,#4095,.F.);
#5282=ORIENTED_EDGE('',*,*,#4096,.F.);
#5283=ORIENTED_EDGE('',*,*,#4095,.T.);
#5284=ORIENTED_EDGE('',*,*,#4097,.F.);
#5285=ORIENTED_EDGE('',*,*,#4098,.F.);
#5286=ORIENTED_EDGE('',*,*,#4099,.F.);
#5287=ORIENTED_EDGE('',*,*,#4098,.T.);
#5288=ORIENTED_EDGE('',*,*,#4100,.F.);
#5289=ORIENTED_EDGE('',*,*,#4101,.F.);
#5290=ORIENTED_EDGE('',*,*,#4102,.F.);
#5291=ORIENTED_EDGE('',*,*,#4101,.T.);
#5292=ORIENTED_EDGE('',*,*,#4103,.F.);
#5293=ORIENTED_EDGE('',*,*,#4104,.F.);
#5294=ORIENTED_EDGE('',*,*,#4105,.F.);
#5295=ORIENTED_EDGE('',*,*,#4104,.T.);
#5296=ORIENTED_EDGE('',*,*,#4106,.F.);
#5297=ORIENTED_EDGE('',*,*,#4107,.F.);
#5298=ORIENTED_EDGE('',*,*,#4108,.F.);
#5299=ORIENTED_EDGE('',*,*,#4107,.T.);
#5300=ORIENTED_EDGE('',*,*,#4109,.F.);
#5301=ORIENTED_EDGE('',*,*,#4110,.F.);
#5302=ORIENTED_EDGE('',*,*,#4111,.F.);
#5303=ORIENTED_EDGE('',*,*,#4110,.T.);
#5304=ORIENTED_EDGE('',*,*,#4112,.F.);
#5305=ORIENTED_EDGE('',*,*,#4113,.F.);
#5306=ORIENTED_EDGE('',*,*,#4114,.F.);
#5307=ORIENTED_EDGE('',*,*,#4113,.T.);
#5308=ORIENTED_EDGE('',*,*,#4115,.F.);
#5309=ORIENTED_EDGE('',*,*,#4116,.F.);
#5310=ORIENTED_EDGE('',*,*,#4117,.F.);
#5311=ORIENTED_EDGE('',*,*,#4116,.T.);
#5312=ORIENTED_EDGE('',*,*,#4118,.F.);
#5313=ORIENTED_EDGE('',*,*,#4119,.F.);
#5314=ORIENTED_EDGE('',*,*,#4120,.F.);
#5315=ORIENTED_EDGE('',*,*,#4119,.T.);
#5316=ORIENTED_EDGE('',*,*,#4121,.F.);
#5317=ORIENTED_EDGE('',*,*,#4069,.F.);
#5318=ORIENTED_EDGE('',*,*,#4120,.T.);
#5319=ORIENTED_EDGE('',*,*,#4068,.T.);
#5320=ORIENTED_EDGE('',*,*,#4072,.T.);
#5321=ORIENTED_EDGE('',*,*,#4075,.T.);
#5322=ORIENTED_EDGE('',*,*,#4078,.T.);
#5323=ORIENTED_EDGE('',*,*,#4081,.T.);
#5324=ORIENTED_EDGE('',*,*,#4084,.T.);
#5325=ORIENTED_EDGE('',*,*,#4087,.T.);
#5326=ORIENTED_EDGE('',*,*,#4090,.T.);
#5327=ORIENTED_EDGE('',*,*,#4093,.T.);
#5328=ORIENTED_EDGE('',*,*,#4096,.T.);
#5329=ORIENTED_EDGE('',*,*,#4099,.T.);
#5330=ORIENTED_EDGE('',*,*,#4102,.T.);
#5331=ORIENTED_EDGE('',*,*,#4105,.T.);
#5332=ORIENTED_EDGE('',*,*,#4108,.T.);
#5333=ORIENTED_EDGE('',*,*,#4111,.T.);
#5334=ORIENTED_EDGE('',*,*,#4114,.T.);
#5335=ORIENTED_EDGE('',*,*,#4117,.T.);
#5336=ORIENTED_EDGE('',*,*,#4070,.T.);
#5337=ORIENTED_EDGE('',*,*,#4122,.T.);
#5338=ORIENTED_EDGE('',*,*,#4073,.T.);
#5339=ORIENTED_EDGE('',*,*,#4123,.T.);
#5340=ORIENTED_EDGE('',*,*,#4076,.T.);
#5341=ORIENTED_EDGE('',*,*,#4124,.T.);
#5342=ORIENTED_EDGE('',*,*,#4079,.T.);
#5343=ORIENTED_EDGE('',*,*,#4125,.T.);
#5344=ORIENTED_EDGE('',*,*,#4082,.T.);
#5345=ORIENTED_EDGE('',*,*,#4126,.T.);
#5346=ORIENTED_EDGE('',*,*,#4085,.T.);
#5347=ORIENTED_EDGE('',*,*,#4127,.T.);
#5348=ORIENTED_EDGE('',*,*,#4088,.T.);
#5349=ORIENTED_EDGE('',*,*,#4128,.T.);
#5350=ORIENTED_EDGE('',*,*,#4091,.T.);
#5351=ORIENTED_EDGE('',*,*,#4129,.T.);
#5352=ORIENTED_EDGE('',*,*,#4094,.T.);
#5353=ORIENTED_EDGE('',*,*,#4130,.T.);
#5354=ORIENTED_EDGE('',*,*,#4131,.T.);
#5355=ORIENTED_EDGE('',*,*,#4132,.T.);
#5356=ORIENTED_EDGE('',*,*,#4133,.T.);
#5357=ORIENTED_EDGE('',*,*,#4134,.T.);
#5358=ORIENTED_EDGE('',*,*,#4135,.T.);
#5359=ORIENTED_EDGE('',*,*,#4136,.T.);
#5360=ORIENTED_EDGE('',*,*,#4137,.T.);
#5361=ORIENTED_EDGE('',*,*,#4138,.T.);
#5362=ORIENTED_EDGE('',*,*,#4139,.T.);
#5363=ORIENTED_EDGE('',*,*,#4140,.T.);
#5364=ORIENTED_EDGE('',*,*,#4141,.T.);
#5365=ORIENTED_EDGE('',*,*,#4142,.T.);
#5366=ORIENTED_EDGE('',*,*,#4143,.T.);
#5367=ORIENTED_EDGE('',*,*,#4144,.T.);
#5368=ORIENTED_EDGE('',*,*,#4145,.T.);
#5369=ORIENTED_EDGE('',*,*,#4146,.T.);
#5370=ORIENTED_EDGE('',*,*,#4147,.T.);
#5371=ORIENTED_EDGE('',*,*,#4148,.T.);
#5372=ORIENTED_EDGE('',*,*,#4149,.T.);
#5373=ORIENTED_EDGE('',*,*,#4150,.T.);
#5374=ORIENTED_EDGE('',*,*,#4151,.T.);
#5375=ORIENTED_EDGE('',*,*,#4152,.T.);
#5376=ORIENTED_EDGE('',*,*,#4153,.T.);
#5377=ORIENTED_EDGE('',*,*,#4121,.T.);
#5378=ORIENTED_EDGE('',*,*,#4118,.T.);
#5379=ORIENTED_EDGE('',*,*,#4115,.T.);
#5380=ORIENTED_EDGE('',*,*,#4112,.T.);
#5381=ORIENTED_EDGE('',*,*,#4109,.T.);
#5382=ORIENTED_EDGE('',*,*,#4106,.T.);
#5383=ORIENTED_EDGE('',*,*,#4103,.T.);
#5384=ORIENTED_EDGE('',*,*,#4100,.T.);
#5385=ORIENTED_EDGE('',*,*,#4097,.T.);
#5386=ORIENTED_EDGE('',*,*,#4067,.T.);
#5387=ORIENTED_EDGE('',*,*,#4154,.F.);
#5388=ORIENTED_EDGE('',*,*,#4155,.T.);
#5389=ORIENTED_EDGE('',*,*,#4156,.F.);
#5390=ORIENTED_EDGE('',*,*,#4157,.F.);
#5391=ORIENTED_EDGE('',*,*,#4158,.F.);
#5392=ORIENTED_EDGE('',*,*,#4157,.T.);
#5393=ORIENTED_EDGE('',*,*,#4159,.F.);
#5394=ORIENTED_EDGE('',*,*,#4160,.F.);
#5395=ORIENTED_EDGE('',*,*,#4161,.F.);
#5396=ORIENTED_EDGE('',*,*,#4160,.T.);
#5397=ORIENTED_EDGE('',*,*,#4162,.F.);
#5398=ORIENTED_EDGE('',*,*,#4163,.F.);
#5399=ORIENTED_EDGE('',*,*,#4164,.F.);
#5400=ORIENTED_EDGE('',*,*,#4163,.T.);
#5401=ORIENTED_EDGE('',*,*,#4165,.F.);
#5402=ORIENTED_EDGE('',*,*,#4166,.F.);
#5403=ORIENTED_EDGE('',*,*,#4167,.F.);
#5404=ORIENTED_EDGE('',*,*,#4166,.T.);
#5405=ORIENTED_EDGE('',*,*,#4168,.F.);
#5406=ORIENTED_EDGE('',*,*,#4169,.F.);
#5407=ORIENTED_EDGE('',*,*,#4170,.F.);
#5408=ORIENTED_EDGE('',*,*,#4169,.T.);
#5409=ORIENTED_EDGE('',*,*,#4171,.F.);
#5410=ORIENTED_EDGE('',*,*,#4172,.F.);
#5411=ORIENTED_EDGE('',*,*,#4173,.F.);
#5412=ORIENTED_EDGE('',*,*,#4172,.T.);
#5413=ORIENTED_EDGE('',*,*,#4174,.F.);
#5414=ORIENTED_EDGE('',*,*,#4175,.F.);
#5415=ORIENTED_EDGE('',*,*,#4176,.F.);
#5416=ORIENTED_EDGE('',*,*,#4175,.T.);
#5417=ORIENTED_EDGE('',*,*,#4177,.F.);
#5418=ORIENTED_EDGE('',*,*,#4178,.F.);
#5419=ORIENTED_EDGE('',*,*,#4179,.F.);
#5420=ORIENTED_EDGE('',*,*,#4178,.T.);
#5421=ORIENTED_EDGE('',*,*,#4151,.F.);
#5422=ORIENTED_EDGE('',*,*,#4180,.F.);
#5423=ORIENTED_EDGE('',*,*,#4181,.F.);
#5424=ORIENTED_EDGE('',*,*,#4180,.T.);
#5425=ORIENTED_EDGE('',*,*,#4150,.F.);
#5426=ORIENTED_EDGE('',*,*,#4182,.F.);
#5427=ORIENTED_EDGE('',*,*,#4183,.F.);
#5428=ORIENTED_EDGE('',*,*,#4182,.T.);
#5429=ORIENTED_EDGE('',*,*,#4149,.F.);
#5430=ORIENTED_EDGE('',*,*,#4184,.F.);
#5431=ORIENTED_EDGE('',*,*,#4185,.F.);
#5432=ORIENTED_EDGE('',*,*,#4184,.T.);
#5433=ORIENTED_EDGE('',*,*,#4148,.F.);
#5434=ORIENTED_EDGE('',*,*,#4186,.F.);
#5435=ORIENTED_EDGE('',*,*,#4187,.F.);
#5436=ORIENTED_EDGE('',*,*,#4186,.T.);
#5437=ORIENTED_EDGE('',*,*,#4147,.F.);
#5438=ORIENTED_EDGE('',*,*,#4188,.F.);
#5439=ORIENTED_EDGE('',*,*,#4189,.F.);
#5440=ORIENTED_EDGE('',*,*,#4188,.T.);
#5441=ORIENTED_EDGE('',*,*,#4146,.F.);
#5442=ORIENTED_EDGE('',*,*,#4190,.F.);
#5443=ORIENTED_EDGE('',*,*,#4191,.F.);
#5444=ORIENTED_EDGE('',*,*,#4190,.T.);
#5445=ORIENTED_EDGE('',*,*,#4145,.F.);
#5446=ORIENTED_EDGE('',*,*,#4192,.F.);
#5447=ORIENTED_EDGE('',*,*,#4193,.F.);
#5448=ORIENTED_EDGE('',*,*,#4192,.T.);
#5449=ORIENTED_EDGE('',*,*,#4144,.F.);
#5450=ORIENTED_EDGE('',*,*,#4194,.F.);
#5451=ORIENTED_EDGE('',*,*,#4195,.F.);
#5452=ORIENTED_EDGE('',*,*,#4194,.T.);
#5453=ORIENTED_EDGE('',*,*,#4143,.F.);
#5454=ORIENTED_EDGE('',*,*,#4196,.F.);
#5455=ORIENTED_EDGE('',*,*,#4197,.F.);
#5456=ORIENTED_EDGE('',*,*,#4196,.T.);
#5457=ORIENTED_EDGE('',*,*,#4142,.F.);
#5458=ORIENTED_EDGE('',*,*,#4155,.F.);
#5459=ORIENTED_EDGE('',*,*,#4197,.T.);
#5460=ORIENTED_EDGE('',*,*,#4154,.T.);
#5461=ORIENTED_EDGE('',*,*,#4158,.T.);
#5462=ORIENTED_EDGE('',*,*,#4161,.T.);
#5463=ORIENTED_EDGE('',*,*,#4164,.T.);
#5464=ORIENTED_EDGE('',*,*,#4167,.T.);
#5465=ORIENTED_EDGE('',*,*,#4170,.T.);
#5466=ORIENTED_EDGE('',*,*,#4173,.T.);
#5467=ORIENTED_EDGE('',*,*,#4176,.T.);
#5468=ORIENTED_EDGE('',*,*,#4179,.T.);
#5469=ORIENTED_EDGE('',*,*,#4181,.T.);
#5470=ORIENTED_EDGE('',*,*,#4183,.T.);
#5471=ORIENTED_EDGE('',*,*,#4185,.T.);
#5472=ORIENTED_EDGE('',*,*,#4187,.T.);
#5473=ORIENTED_EDGE('',*,*,#4189,.T.);
#5474=ORIENTED_EDGE('',*,*,#4191,.T.);
#5475=ORIENTED_EDGE('',*,*,#4193,.T.);
#5476=ORIENTED_EDGE('',*,*,#4195,.T.);
#5477=ORIENTED_EDGE('',*,*,#4156,.T.);
#5478=ORIENTED_EDGE('',*,*,#4198,.T.);
#5479=ORIENTED_EDGE('',*,*,#4159,.T.);
#5480=ORIENTED_EDGE('',*,*,#4199,.T.);
#5481=ORIENTED_EDGE('',*,*,#4162,.T.);
#5482=ORIENTED_EDGE('',*,*,#4200,.T.);
#5483=ORIENTED_EDGE('',*,*,#4165,.T.);
#5484=ORIENTED_EDGE('',*,*,#4201,.T.);
#5485=ORIENTED_EDGE('',*,*,#4168,.T.);
#5486=ORIENTED_EDGE('',*,*,#4202,.T.);
#5487=ORIENTED_EDGE('',*,*,#4171,.T.);
#5488=ORIENTED_EDGE('',*,*,#4203,.T.);
#5489=ORIENTED_EDGE('',*,*,#4174,.T.);
#5490=ORIENTED_EDGE('',*,*,#4204,.T.);
#5491=ORIENTED_EDGE('',*,*,#4177,.T.);
#5492=ORIENTED_EDGE('',*,*,#4205,.T.);
#5493=ORIENTED_EDGE('',*,*,#4206,.F.);
#5494=ORIENTED_EDGE('',*,*,#4207,.T.);
#5495=ORIENTED_EDGE('',*,*,#4208,.F.);
#5496=ORIENTED_EDGE('',*,*,#4209,.F.);
#5497=ORIENTED_EDGE('',*,*,#4210,.F.);
#5498=ORIENTED_EDGE('',*,*,#4209,.T.);
#5499=ORIENTED_EDGE('',*,*,#4211,.F.);
#5500=ORIENTED_EDGE('',*,*,#4212,.F.);
#5501=ORIENTED_EDGE('',*,*,#4213,.F.);
#5502=ORIENTED_EDGE('',*,*,#4212,.T.);
#5503=ORIENTED_EDGE('',*,*,#4214,.F.);
#5504=ORIENTED_EDGE('',*,*,#4215,.F.);
#5505=ORIENTED_EDGE('',*,*,#4216,.F.);
#5506=ORIENTED_EDGE('',*,*,#4215,.T.);
#5507=ORIENTED_EDGE('',*,*,#4217,.F.);
#5508=ORIENTED_EDGE('',*,*,#4218,.F.);
#5509=ORIENTED_EDGE('',*,*,#4219,.F.);
#5510=ORIENTED_EDGE('',*,*,#4218,.T.);
#5511=ORIENTED_EDGE('',*,*,#4220,.F.);
#5512=ORIENTED_EDGE('',*,*,#4221,.F.);
#5513=ORIENTED_EDGE('',*,*,#4222,.F.);
#5514=ORIENTED_EDGE('',*,*,#4221,.T.);
#5515=ORIENTED_EDGE('',*,*,#4223,.F.);
#5516=ORIENTED_EDGE('',*,*,#4224,.F.);
#5517=ORIENTED_EDGE('',*,*,#4225,.F.);
#5518=ORIENTED_EDGE('',*,*,#4224,.T.);
#5519=ORIENTED_EDGE('',*,*,#4226,.F.);
#5520=ORIENTED_EDGE('',*,*,#4227,.F.);
#5521=ORIENTED_EDGE('',*,*,#4228,.F.);
#5522=ORIENTED_EDGE('',*,*,#4227,.T.);
#5523=ORIENTED_EDGE('',*,*,#4229,.F.);
#5524=ORIENTED_EDGE('',*,*,#4230,.F.);
#5525=ORIENTED_EDGE('',*,*,#4231,.F.);
#5526=ORIENTED_EDGE('',*,*,#4230,.T.);
#5527=ORIENTED_EDGE('',*,*,#4140,.F.);
#5528=ORIENTED_EDGE('',*,*,#4232,.F.);
#5529=ORIENTED_EDGE('',*,*,#4233,.F.);
#5530=ORIENTED_EDGE('',*,*,#4232,.T.);
#5531=ORIENTED_EDGE('',*,*,#4139,.F.);
#5532=ORIENTED_EDGE('',*,*,#4234,.F.);
#5533=ORIENTED_EDGE('',*,*,#4235,.F.);
#5534=ORIENTED_EDGE('',*,*,#4234,.T.);
#5535=ORIENTED_EDGE('',*,*,#4138,.F.);
#5536=ORIENTED_EDGE('',*,*,#4236,.F.);
#5537=ORIENTED_EDGE('',*,*,#4237,.F.);
#5538=ORIENTED_EDGE('',*,*,#4236,.T.);
#5539=ORIENTED_EDGE('',*,*,#4137,.F.);
#5540=ORIENTED_EDGE('',*,*,#4238,.F.);
#5541=ORIENTED_EDGE('',*,*,#4239,.F.);
#5542=ORIENTED_EDGE('',*,*,#4238,.T.);
#5543=ORIENTED_EDGE('',*,*,#4136,.F.);
#5544=ORIENTED_EDGE('',*,*,#4240,.F.);
#5545=ORIENTED_EDGE('',*,*,#4241,.F.);
#5546=ORIENTED_EDGE('',*,*,#4240,.T.);
#5547=ORIENTED_EDGE('',*,*,#4135,.F.);
#5548=ORIENTED_EDGE('',*,*,#4242,.F.);
#5549=ORIENTED_EDGE('',*,*,#4243,.F.);
#5550=ORIENTED_EDGE('',*,*,#4242,.T.);
#5551=ORIENTED_EDGE('',*,*,#4134,.F.);
#5552=ORIENTED_EDGE('',*,*,#4244,.F.);
#5553=ORIENTED_EDGE('',*,*,#4245,.F.);
#5554=ORIENTED_EDGE('',*,*,#4244,.T.);
#5555=ORIENTED_EDGE('',*,*,#4133,.F.);
#5556=ORIENTED_EDGE('',*,*,#4246,.F.);
#5557=ORIENTED_EDGE('',*,*,#4247,.F.);
#5558=ORIENTED_EDGE('',*,*,#4246,.T.);
#5559=ORIENTED_EDGE('',*,*,#4132,.F.);
#5560=ORIENTED_EDGE('',*,*,#4248,.F.);
#5561=ORIENTED_EDGE('',*,*,#4249,.F.);
#5562=ORIENTED_EDGE('',*,*,#4248,.T.);
#5563=ORIENTED_EDGE('',*,*,#4131,.F.);
#5564=ORIENTED_EDGE('',*,*,#4207,.F.);
#5565=ORIENTED_EDGE('',*,*,#4249,.T.);
#5566=ORIENTED_EDGE('',*,*,#4206,.T.);
#5567=ORIENTED_EDGE('',*,*,#4210,.T.);
#5568=ORIENTED_EDGE('',*,*,#4213,.T.);
#5569=ORIENTED_EDGE('',*,*,#4216,.T.);
#5570=ORIENTED_EDGE('',*,*,#4219,.T.);
#5571=ORIENTED_EDGE('',*,*,#4222,.T.);
#5572=ORIENTED_EDGE('',*,*,#4225,.T.);
#5573=ORIENTED_EDGE('',*,*,#4228,.T.);
#5574=ORIENTED_EDGE('',*,*,#4231,.T.);
#5575=ORIENTED_EDGE('',*,*,#4233,.T.);
#5576=ORIENTED_EDGE('',*,*,#4235,.T.);
#5577=ORIENTED_EDGE('',*,*,#4237,.T.);
#5578=ORIENTED_EDGE('',*,*,#4239,.T.);
#5579=ORIENTED_EDGE('',*,*,#4241,.T.);
#5580=ORIENTED_EDGE('',*,*,#4243,.T.);
#5581=ORIENTED_EDGE('',*,*,#4245,.T.);
#5582=ORIENTED_EDGE('',*,*,#4247,.T.);
#5583=ORIENTED_EDGE('',*,*,#4208,.T.);
#5584=ORIENTED_EDGE('',*,*,#4250,.T.);
#5585=ORIENTED_EDGE('',*,*,#4211,.T.);
#5586=ORIENTED_EDGE('',*,*,#4251,.T.);
#5587=ORIENTED_EDGE('',*,*,#4214,.T.);
#5588=ORIENTED_EDGE('',*,*,#4252,.T.);
#5589=ORIENTED_EDGE('',*,*,#4217,.T.);
#5590=ORIENTED_EDGE('',*,*,#4253,.T.);
#5591=ORIENTED_EDGE('',*,*,#4220,.T.);
#5592=ORIENTED_EDGE('',*,*,#4254,.T.);
#5593=ORIENTED_EDGE('',*,*,#4223,.T.);
#5594=ORIENTED_EDGE('',*,*,#4255,.T.);
#5595=ORIENTED_EDGE('',*,*,#4226,.T.);
#5596=ORIENTED_EDGE('',*,*,#4256,.T.);
#5597=ORIENTED_EDGE('',*,*,#4229,.T.);
#5598=ORIENTED_EDGE('',*,*,#4257,.T.);
#5599=ORIENTED_EDGE('',*,*,#4258,.F.);
#5600=ORIENTED_EDGE('',*,*,#4259,.T.);
#5601=ORIENTED_EDGE('',*,*,#4152,.F.);
#5602=ORIENTED_EDGE('',*,*,#4205,.F.);
#5603=ORIENTED_EDGE('',*,*,#4204,.F.);
#5604=ORIENTED_EDGE('',*,*,#4203,.F.);
#5605=ORIENTED_EDGE('',*,*,#4202,.F.);
#5606=ORIENTED_EDGE('',*,*,#4201,.F.);
#5607=ORIENTED_EDGE('',*,*,#4200,.F.);
#5608=ORIENTED_EDGE('',*,*,#4199,.F.);
#5609=ORIENTED_EDGE('',*,*,#4198,.F.);
#5610=ORIENTED_EDGE('',*,*,#4141,.F.);
#5611=ORIENTED_EDGE('',*,*,#4257,.F.);
#5612=ORIENTED_EDGE('',*,*,#4256,.F.);
#5613=ORIENTED_EDGE('',*,*,#4255,.F.);
#5614=ORIENTED_EDGE('',*,*,#4254,.F.);
#5615=ORIENTED_EDGE('',*,*,#4253,.F.);
#5616=ORIENTED_EDGE('',*,*,#4252,.F.);
#5617=ORIENTED_EDGE('',*,*,#4251,.F.);
#5618=ORIENTED_EDGE('',*,*,#4250,.F.);
#5619=ORIENTED_EDGE('',*,*,#4130,.F.);
#5620=ORIENTED_EDGE('',*,*,#4129,.F.);
#5621=ORIENTED_EDGE('',*,*,#4128,.F.);
#5622=ORIENTED_EDGE('',*,*,#4127,.F.);
#5623=ORIENTED_EDGE('',*,*,#4126,.F.);
#5624=ORIENTED_EDGE('',*,*,#4125,.F.);
#5625=ORIENTED_EDGE('',*,*,#4124,.F.);
#5626=ORIENTED_EDGE('',*,*,#4123,.F.);
#5627=ORIENTED_EDGE('',*,*,#4122,.F.);
#5628=ORIENTED_EDGE('',*,*,#4153,.F.);
#5629=ORIENTED_EDGE('',*,*,#4259,.F.);
#5630=ORIENTED_EDGE('',*,*,#4064,.T.);
#5631=ORIENTED_EDGE('',*,*,#4258,.T.);
#5632=ORIENTED_EDGE('',*,*,#4065,.T.);
#6931=CYLINDRICAL_SURFACE('',#7618,0.21);
#6932=CYLINDRICAL_SURFACE('',#7619,0.6);
#6933=CYLINDRICAL_SURFACE('',#7732,1.37);
#7023=ADVANCED_FACE('',(#632),#6931,.F.);
#7024=ADVANCED_FACE('',(#633,#185),#6932,.F.);
#7025=ADVANCED_FACE('',(#634),#244,.T.);
#7026=ADVANCED_FACE('',(#635),#245,.T.);
#7027=ADVANCED_FACE('',(#636),#246,.T.);
#7028=ADVANCED_FACE('',(#637),#247,.T.);
#7029=ADVANCED_FACE('',(#638),#248,.T.);
#7030=ADVANCED_FACE('',(#639),#249,.T.);
#7031=ADVANCED_FACE('',(#640),#250,.T.);
#7032=ADVANCED_FACE('',(#641),#251,.T.);
#7033=ADVANCED_FACE('',(#642),#252,.T.);
#7034=ADVANCED_FACE('',(#643),#253,.T.);
#7035=ADVANCED_FACE('',(#644),#254,.T.);
#7036=ADVANCED_FACE('',(#645),#255,.T.);
#7037=ADVANCED_FACE('',(#646),#256,.T.);
#7038=ADVANCED_FACE('',(#647),#257,.T.);
#7039=ADVANCED_FACE('',(#648),#258,.T.);
#7040=ADVANCED_FACE('',(#649),#259,.T.);
#7041=ADVANCED_FACE('',(#650),#260,.T.);
#7042=ADVANCED_FACE('',(#651),#261,.T.);
#7043=ADVANCED_FACE('',(#652),#262,.T.);
#7044=ADVANCED_FACE('',(#653),#263,.T.);
#7045=ADVANCED_FACE('',(#654),#264,.T.);
#7046=ADVANCED_FACE('',(#655),#265,.T.);
#7047=ADVANCED_FACE('',(#656),#266,.T.);
#7048=ADVANCED_FACE('',(#657),#267,.T.);
#7049=ADVANCED_FACE('',(#658),#268,.T.);
#7050=ADVANCED_FACE('',(#659),#269,.T.);
#7051=ADVANCED_FACE('',(#660),#270,.T.);
#7052=ADVANCED_FACE('',(#661,#186),#271,.T.);
#7053=ADVANCED_FACE('',(#662),#272,.T.);
#7054=ADVANCED_FACE('',(#663),#273,.T.);
#7055=ADVANCED_FACE('',(#664),#274,.T.);
#7056=ADVANCED_FACE('',(#665),#275,.T.);
#7057=ADVANCED_FACE('',(#666),#276,.T.);
#7058=ADVANCED_FACE('',(#667),#277,.T.);
#7059=ADVANCED_FACE('',(#668),#278,.T.);
#7060=ADVANCED_FACE('',(#669),#279,.T.);
#7061=ADVANCED_FACE('',(#670),#280,.T.);
#7062=ADVANCED_FACE('',(#671),#281,.T.);
#7063=ADVANCED_FACE('',(#672),#282,.T.);
#7064=ADVANCED_FACE('',(#673),#283,.T.);
#7065=ADVANCED_FACE('',(#674),#284,.T.);
#7066=ADVANCED_FACE('',(#675),#285,.T.);
#7067=ADVANCED_FACE('',(#676),#286,.T.);
#7068=ADVANCED_FACE('',(#677),#287,.T.);
#7069=ADVANCED_FACE('',(#678),#288,.T.);
#7070=ADVANCED_FACE('',(#679),#289,.T.);
#7071=ADVANCED_FACE('',(#680),#290,.T.);
#7072=ADVANCED_FACE('',(#681),#291,.T.);
#7073=ADVANCED_FACE('',(#682),#292,.T.);
#7074=ADVANCED_FACE('',(#683),#293,.T.);
#7075=ADVANCED_FACE('',(#684),#294,.T.);
#7076=ADVANCED_FACE('',(#685),#295,.T.);
#7077=ADVANCED_FACE('',(#686),#296,.T.);
#7078=ADVANCED_FACE('',(#687),#297,.T.);
#7079=ADVANCED_FACE('',(#688),#298,.T.);
#7080=ADVANCED_FACE('',(#689),#299,.T.);
#7081=ADVANCED_FACE('',(#690),#300,.T.);
#7082=ADVANCED_FACE('',(#691),#301,.T.);
#7083=ADVANCED_FACE('',(#692),#302,.T.);
#7084=ADVANCED_FACE('',(#693),#303,.T.);
#7085=ADVANCED_FACE('',(#694),#304,.T.);
#7086=ADVANCED_FACE('',(#695),#305,.T.);
#7087=ADVANCED_FACE('',(#696),#306,.T.);
#7088=ADVANCED_FACE('',(#697),#307,.T.);
#7089=ADVANCED_FACE('',(#698),#308,.T.);
#7090=ADVANCED_FACE('',(#699),#309,.T.);
#7091=ADVANCED_FACE('',(#700),#310,.T.);
#7092=ADVANCED_FACE('',(#701),#311,.T.);
#7093=ADVANCED_FACE('',(#702),#312,.T.);
#7094=ADVANCED_FACE('',(#703),#313,.T.);
#7095=ADVANCED_FACE('',(#704),#314,.T.);
#7096=ADVANCED_FACE('',(#705),#315,.T.);
#7097=ADVANCED_FACE('',(#706),#316,.T.);
#7098=ADVANCED_FACE('',(#707),#317,.T.);
#7099=ADVANCED_FACE('',(#708),#318,.T.);
#7100=ADVANCED_FACE('',(#709),#319,.T.);
#7101=ADVANCED_FACE('',(#710),#320,.T.);
#7102=ADVANCED_FACE('',(#711),#321,.T.);
#7103=ADVANCED_FACE('',(#712),#322,.T.);
#7104=ADVANCED_FACE('',(#713),#323,.T.);
#7105=ADVANCED_FACE('',(#714),#324,.T.);
#7106=ADVANCED_FACE('',(#715),#325,.T.);
#7107=ADVANCED_FACE('',(#716,#187),#6933,.T.);
#7108=ADVANCED_FACE('',(#717,#188),#326,.F.);
#7356=CLOSED_SHELL('',(#7023,#7024,#7025,#7026,#7027,#7028,#7029,#7030,
#7031,#7032,#7033,#7034,#7035,#7036,#7037,#7038,#7039,#7040,#7041,#7042,
#7043,#7044,#7045,#7046,#7047,#7048,#7049,#7050,#7051,#7052,#7053,#7054,
#7055,#7056,#7057,#7058,#7059,#7060,#7061,#7062,#7063,#7064,#7065,#7066,
#7067,#7068,#7069,#7070,#7071,#7072,#7073,#7074,#7075,#7076,#7077,#7078,
#7079,#7080,#7081,#7082,#7083,#7084,#7085,#7086,#7087,#7088,#7089,#7090,
#7091,#7092,#7093,#7094,#7095,#7096,#7097,#7098,#7099,#7100,#7101,#7102,
#7103,#7104,#7105,#7106,#7107,#7108));
#7617=AXIS2_PLACEMENT_3D('',#10471,#8433,#8434);
#7618=AXIS2_PLACEMENT_3D('',#10472,#8435,#8436);
#7619=AXIS2_PLACEMENT_3D('',#10547,#8438,#8439);
#7620=AXIS2_PLACEMENT_3D('',#10549,#8440,#8441);
#7621=AXIS2_PLACEMENT_3D('',#10552,#8443,#8444);
#7622=AXIS2_PLACEMENT_3D('',#10553,#8445,#8446);
#7623=AXIS2_PLACEMENT_3D('',#10562,#8451,#8452);
#7624=AXIS2_PLACEMENT_3D('',#10568,#8456,#8457);
#7625=AXIS2_PLACEMENT_3D('',#10574,#8461,#8462);
#7626=AXIS2_PLACEMENT_3D('',#10580,#8466,#8467);
#7627=AXIS2_PLACEMENT_3D('',#10586,#8471,#8472);
#7628=AXIS2_PLACEMENT_3D('',#10592,#8476,#8477);
#7629=AXIS2_PLACEMENT_3D('',#10598,#8481,#8482);
#7630=AXIS2_PLACEMENT_3D('',#10604,#8486,#8487);
#7631=AXIS2_PLACEMENT_3D('',#10610,#8491,#8492);
#7632=AXIS2_PLACEMENT_3D('',#10616,#8496,#8497);
#7633=AXIS2_PLACEMENT_3D('',#10622,#8501,#8502);
#7634=AXIS2_PLACEMENT_3D('',#10628,#8506,#8507);
#7635=AXIS2_PLACEMENT_3D('',#10634,#8511,#8512);
#7636=AXIS2_PLACEMENT_3D('',#10640,#8516,#8517);
#7637=AXIS2_PLACEMENT_3D('',#10646,#8521,#8522);
#7638=AXIS2_PLACEMENT_3D('',#10652,#8526,#8527);
#7639=AXIS2_PLACEMENT_3D('',#10658,#8531,#8532);
#7640=AXIS2_PLACEMENT_3D('',#10661,#8535,#8536);
#7641=AXIS2_PLACEMENT_3D('',#10662,#8537,#8538);
#7642=AXIS2_PLACEMENT_3D('',#10663,#8539,#8540);
#7643=AXIS2_PLACEMENT_3D('',#10664,#8541,#8542);
#7644=AXIS2_PLACEMENT_3D('',#10665,#8543,#8544);
#7645=AXIS2_PLACEMENT_3D('',#10666,#8545,#8546);
#7646=AXIS2_PLACEMENT_3D('',#10667,#8547,#8548);
#7647=AXIS2_PLACEMENT_3D('',#10668,#8549,#8550);
#7648=AXIS2_PLACEMENT_3D('',#10669,#8551,#8552);
#7649=AXIS2_PLACEMENT_3D('',#10670,#8553,#8554);
#7650=AXIS2_PLACEMENT_3D('',#10671,#8555,#8556);
#7651=AXIS2_PLACEMENT_3D('',#10672,#8557,#8558);
#7652=AXIS2_PLACEMENT_3D('',#10673,#8559,#8560);
#7653=AXIS2_PLACEMENT_3D('',#10674,#8561,#8562);
#7654=AXIS2_PLACEMENT_3D('',#10675,#8563,#8564);
#7655=AXIS2_PLACEMENT_3D('',#10676,#8565,#8566);
#7656=AXIS2_PLACEMENT_3D('',#10677,#8567,#8568);
#7657=AXIS2_PLACEMENT_3D('',#10678,#8569,#8570);
#7658=AXIS2_PLACEMENT_3D('',#10680,#8571,#8572);
#7659=AXIS2_PLACEMENT_3D('',#10702,#8583,#8584);
#7660=AXIS2_PLACEMENT_3D('',#10724,#8595,#8596);
#7661=AXIS2_PLACEMENT_3D('',#10725,#8597,#8598);
#7662=AXIS2_PLACEMENT_3D('',#10726,#8599,#8600);
#7663=AXIS2_PLACEMENT_3D('',#10734,#8605,#8606);
#7664=AXIS2_PLACEMENT_3D('',#10740,#8610,#8611);
#7665=AXIS2_PLACEMENT_3D('',#10746,#8615,#8616);
#7666=AXIS2_PLACEMENT_3D('',#10752,#8620,#8621);
#7667=AXIS2_PLACEMENT_3D('',#10758,#8625,#8626);
#7668=AXIS2_PLACEMENT_3D('',#10764,#8630,#8631);
#7669=AXIS2_PLACEMENT_3D('',#10770,#8635,#8636);
#7670=AXIS2_PLACEMENT_3D('',#10775,#8640,#8641);
#7671=AXIS2_PLACEMENT_3D('',#10779,#8644,#8645);
#7672=AXIS2_PLACEMENT_3D('',#10783,#8648,#8649);
#7673=AXIS2_PLACEMENT_3D('',#10787,#8652,#8653);
#7674=AXIS2_PLACEMENT_3D('',#10791,#8656,#8657);
#7675=AXIS2_PLACEMENT_3D('',#10795,#8660,#8661);
#7676=AXIS2_PLACEMENT_3D('',#10799,#8664,#8665);
#7677=AXIS2_PLACEMENT_3D('',#10803,#8668,#8669);
#7678=AXIS2_PLACEMENT_3D('',#10807,#8672,#8673);
#7679=AXIS2_PLACEMENT_3D('',#10811,#8676,#8677);
#7680=AXIS2_PLACEMENT_3D('',#10813,#8679,#8680);
#7681=AXIS2_PLACEMENT_3D('',#10814,#8681,#8682);
#7682=AXIS2_PLACEMENT_3D('',#10815,#8683,#8684);
#7683=AXIS2_PLACEMENT_3D('',#10816,#8685,#8686);
#7684=AXIS2_PLACEMENT_3D('',#10817,#8687,#8688);
#7685=AXIS2_PLACEMENT_3D('',#10818,#8689,#8690);
#7686=AXIS2_PLACEMENT_3D('',#10819,#8691,#8692);
#7687=AXIS2_PLACEMENT_3D('',#10820,#8693,#8694);
#7688=AXIS2_PLACEMENT_3D('',#10821,#8695,#8696);
#7689=AXIS2_PLACEMENT_3D('',#10822,#8697,#8698);
#7690=AXIS2_PLACEMENT_3D('',#10823,#8699,#8700);
#7691=AXIS2_PLACEMENT_3D('',#10824,#8701,#8702);
#7692=AXIS2_PLACEMENT_3D('',#10825,#8703,#8704);
#7693=AXIS2_PLACEMENT_3D('',#10826,#8705,#8706);
#7694=AXIS2_PLACEMENT_3D('',#10827,#8707,#8708);
#7695=AXIS2_PLACEMENT_3D('',#10828,#8709,#8710);
#7696=AXIS2_PLACEMENT_3D('',#10829,#8711,#8712);
#7697=AXIS2_PLACEMENT_3D('',#10830,#8713,#8714);
#7698=AXIS2_PLACEMENT_3D('',#10838,#8719,#8720);
#7699=AXIS2_PLACEMENT_3D('',#10844,#8724,#8725);
#7700=AXIS2_PLACEMENT_3D('',#10850,#8729,#8730);
#7701=AXIS2_PLACEMENT_3D('',#10856,#8734,#8735);
#7702=AXIS2_PLACEMENT_3D('',#10862,#8739,#8740);
#7703=AXIS2_PLACEMENT_3D('',#10868,#8744,#8745);
#7704=AXIS2_PLACEMENT_3D('',#10874,#8749,#8750);
#7705=AXIS2_PLACEMENT_3D('',#10879,#8754,#8755);
#7706=AXIS2_PLACEMENT_3D('',#10883,#8758,#8759);
#7707=AXIS2_PLACEMENT_3D('',#10887,#8762,#8763);
#7708=AXIS2_PLACEMENT_3D('',#10891,#8766,#8767);
#7709=AXIS2_PLACEMENT_3D('',#10895,#8770,#8771);
#7710=AXIS2_PLACEMENT_3D('',#10899,#8774,#8775);
#7711=AXIS2_PLACEMENT_3D('',#10903,#8778,#8779);
#7712=AXIS2_PLACEMENT_3D('',#10907,#8782,#8783);
#7713=AXIS2_PLACEMENT_3D('',#10911,#8786,#8787);
#7714=AXIS2_PLACEMENT_3D('',#10915,#8790,#8791);
#7715=AXIS2_PLACEMENT_3D('',#10917,#8793,#8794);
#7716=AXIS2_PLACEMENT_3D('',#10918,#8795,#8796);
#7717=AXIS2_PLACEMENT_3D('',#10919,#8797,#8798);
#7718=AXIS2_PLACEMENT_3D('',#10920,#8799,#8800);
#7719=AXIS2_PLACEMENT_3D('',#10921,#8801,#8802);
#7720=AXIS2_PLACEMENT_3D('',#10922,#8803,#8804);
#7721=AXIS2_PLACEMENT_3D('',#10923,#8805,#8806);
#7722=AXIS2_PLACEMENT_3D('',#10924,#8807,#8808);
#7723=AXIS2_PLACEMENT_3D('',#10925,#8809,#8810);
#7724=AXIS2_PLACEMENT_3D('',#10926,#8811,#8812);
#7725=AXIS2_PLACEMENT_3D('',#10927,#8813,#8814);
#7726=AXIS2_PLACEMENT_3D('',#10928,#8815,#8816);
#7727=AXIS2_PLACEMENT_3D('',#10929,#8817,#8818);
#7728=AXIS2_PLACEMENT_3D('',#10930,#8819,#8820);
#7729=AXIS2_PLACEMENT_3D('',#10931,#8821,#8822);
#7730=AXIS2_PLACEMENT_3D('',#10932,#8823,#8824);
#7731=AXIS2_PLACEMENT_3D('',#10933,#8825,#8826);
#7732=AXIS2_PLACEMENT_3D('',#10934,#8827,#8828);
#7733=AXIS2_PLACEMENT_3D('',#10936,#8829,#8830);
#7734=AXIS2_PLACEMENT_3D('',#10938,#8832,#8833);
#8433=DIRECTION('axis',(0.,0.,1.));
#8434=DIRECTION('refdir',(1.,0.,0.));
#8435=DIRECTION('center_axis',(0.,0.,1.));
#8436=DIRECTION('ref_axis',(1.,0.,0.));
#8437=DIRECTION('',(0.,0.,1.));
#8438=DIRECTION('center_axis',(0.,1.,0.));
#8439=DIRECTION('ref_axis',(1.,0.,0.));
#8440=DIRECTION('center_axis',(0.,1.,0.));
#8441=DIRECTION('ref_axis',(1.,0.,0.));
#8442=DIRECTION('',(0.,1.,0.));
#8443=DIRECTION('center_axis',(0.,-1.,0.));
#8444=DIRECTION('ref_axis',(1.,0.,0.));
#8445=DIRECTION('center_axis',(-0.762527203906389,0.,0.646956152534856));
#8446=DIRECTION('ref_axis',(-0.646956152534856,0.,-0.762527203906389));
#8447=DIRECTION('',(0.646956152534856,0.,0.762527203906389));
#8448=DIRECTION('',(0.,-1.,0.));
#8449=DIRECTION('',(-0.646956152534856,0.,-0.762527203906389));
#8450=DIRECTION('',(0.,-1.,0.));
#8451=DIRECTION('center_axis',(-0.695442635009613,0.,0.718581617779697));
#8452=DIRECTION('ref_axis',(-0.718581617779697,0.,-0.695442635009613));
#8453=DIRECTION('',(0.718581617779697,0.,0.695442635009613));
#8454=DIRECTION('',(-0.718581617779697,0.,-0.695442635009613));
#8455=DIRECTION('',(0.,-1.,0.));
#8456=DIRECTION('center_axis',(-0.621660573370079,0.,0.783286749228649));
#8457=DIRECTION('ref_axis',(-0.783286749228649,0.,-0.621660573370079));
#8458=DIRECTION('',(0.783286749228649,0.,0.621660573370079));
#8459=DIRECTION('',(-0.783286749228649,0.,-0.621660573370079));
#8460=DIRECTION('',(0.,-1.,0.));
#8461=DIRECTION('center_axis',(-0.541891580574751,0.,0.840448401094439));
#8462=DIRECTION('ref_axis',(-0.840448401094439,0.,-0.541891580574751));
#8463=DIRECTION('',(0.840448401094439,0.,0.541891580574751));
#8464=DIRECTION('',(-0.840448401094439,0.,-0.541891580574751));
#8465=DIRECTION('',(0.,-1.,0.));
#8466=DIRECTION('center_axis',(-0.456903875630423,0.,0.889516075421855));
#8467=DIRECTION('ref_axis',(-0.889516075421855,0.,-0.456903875630423));
#8468=DIRECTION('',(0.889516075421855,0.,0.456903875630423));
#8469=DIRECTION('',(-0.889516075421855,0.,-0.456903875630423));
#8470=DIRECTION('',(0.,-1.,0.));
#8471=DIRECTION('center_axis',(-0.367515936594703,0.,0.930017223684012));
#8472=DIRECTION('ref_axis',(-0.930017223684012,0.,-0.367515936594703));
#8473=DIRECTION('',(0.930017223684012,0.,0.367515936594703));
#8474=DIRECTION('',(-0.930017223684012,0.,-0.367515936594703));
#8475=DIRECTION('',(0.,-1.,0.));
#8476=DIRECTION('center_axis',(-0.274588618184932,0.,0.961561797682962));
#8477=DIRECTION('ref_axis',(-0.961561797682962,0.,-0.274588618184932));
#8478=DIRECTION('',(0.961561797682962,0.,0.274588618184932));
#8479=DIRECTION('',(-0.961561797682962,0.,-0.274588618184932));
#8480=DIRECTION('',(0.,-1.,0.));
#8481=DIRECTION('center_axis',(-0.179016861276632,0.,0.983846005927077));
#8482=DIRECTION('ref_axis',(-0.983846005927077,0.,-0.179016861276632));
#8483=DIRECTION('',(0.983846005927077,0.,0.179016861276632));
#8484=DIRECTION('',(-0.983846005927077,0.,-0.179016861276632));
#8485=DIRECTION('',(0.,-1.,0.));
#8486=DIRECTION('center_axis',(0.99144486137381,0.,0.130526192220052));
#8487=DIRECTION('ref_axis',(-0.130526192220052,0.,0.99144486137381));
#8488=DIRECTION('',(0.130526192220052,0.,-0.99144486137381));
#8489=DIRECTION('',(-0.130526192220052,0.,0.99144486137381));
#8490=DIRECTION('',(0.,-1.,0.));
#8491=DIRECTION('center_axis',(0.179016861276633,0.,-0.983846005927077));
#8492=DIRECTION('ref_axis',(0.983846005927077,0.,0.179016861276633));
#8493=DIRECTION('',(-0.983846005927077,0.,-0.179016861276633));
#8494=DIRECTION('',(0.983846005927077,0.,0.179016861276633));
#8495=DIRECTION('',(0.,-1.,0.));
#8496=DIRECTION('center_axis',(0.274588618184932,0.,-0.961561797682962));
#8497=DIRECTION('ref_axis',(0.961561797682962,0.,0.274588618184932));
#8498=DIRECTION('',(-0.961561797682962,0.,-0.274588618184932));
#8499=DIRECTION('',(0.961561797682962,0.,0.274588618184932));
#8500=DIRECTION('',(0.,-1.,0.));
#8501=DIRECTION('center_axis',(0.367515936594704,0.,-0.930017223684012));
#8502=DIRECTION('ref_axis',(0.930017223684012,0.,0.367515936594704));
#8503=DIRECTION('',(-0.930017223684012,0.,-0.367515936594704));
#8504=DIRECTION('',(0.930017223684012,0.,0.367515936594704));
#8505=DIRECTION('',(0.,-1.,0.));
#8506=DIRECTION('center_axis',(0.456903875630421,0.,-0.889516075421856));
#8507=DIRECTION('ref_axis',(0.889516075421856,0.,0.456903875630421));
#8508=DIRECTION('',(-0.889516075421856,0.,-0.456903875630421));
#8509=DIRECTION('',(0.889516075421856,0.,0.456903875630421));
#8510=DIRECTION('',(0.,-1.,0.));
#8511=DIRECTION('center_axis',(0.541891580574752,0.,-0.840448401094438));
#8512=DIRECTION('ref_axis',(0.840448401094438,0.,0.541891580574752));
#8513=DIRECTION('',(-0.840448401094438,0.,-0.541891580574752));
#8514=DIRECTION('',(0.840448401094438,0.,0.541891580574752));
#8515=DIRECTION('',(0.,-1.,0.));
#8516=DIRECTION('center_axis',(0.621660573370078,0.,-0.78328674922865));
#8517=DIRECTION('ref_axis',(0.78328674922865,0.,0.621660573370078));
#8518=DIRECTION('',(-0.78328674922865,0.,-0.621660573370078));
#8519=DIRECTION('',(0.78328674922865,0.,0.621660573370078));
#8520=DIRECTION('',(0.,-1.,0.));
#8521=DIRECTION('center_axis',(0.695442635009612,0.,-0.718581617779697));
#8522=DIRECTION('ref_axis',(0.718581617779697,0.,0.695442635009612));
#8523=DIRECTION('',(-0.718581617779697,0.,-0.695442635009612));
#8524=DIRECTION('',(0.718581617779697,0.,0.695442635009612));
#8525=DIRECTION('',(0.,-1.,0.));
#8526=DIRECTION('center_axis',(0.762527203906389,0.,-0.646956152534857));
#8527=DIRECTION('ref_axis',(0.646956152534857,0.,0.762527203906389));
#8528=DIRECTION('',(-0.646956152534857,0.,-0.762527203906389));
#8529=DIRECTION('',(0.646956152534857,0.,0.762527203906389));
#8530=DIRECTION('',(0.,-1.,0.));
#8531=DIRECTION('center_axis',(-0.60876142900872,0.,-0.793353340291236));
#8532=DIRECTION('ref_axis',(0.793353340291236,0.,-0.60876142900872));
#8533=DIRECTION('',(-0.793353340291236,0.,0.60876142900872));
#8534=DIRECTION('',(0.793353340291236,0.,-0.60876142900872));
#8535=DIRECTION('center_axis',(0.,1.,0.));
#8536=DIRECTION('ref_axis',(-0.5,0.,0.866025403784438));
#8537=DIRECTION('center_axis',(0.,1.,0.));
#8538=DIRECTION('ref_axis',(1.,0.,0.));
#8539=DIRECTION('center_axis',(0.,1.,0.));
#8540=DIRECTION('ref_axis',(1.,0.,0.));
#8541=DIRECTION('center_axis',(0.,1.,0.));
#8542=DIRECTION('ref_axis',(1.,0.,0.));
#8543=DIRECTION('center_axis',(0.,1.,0.));
#8544=DIRECTION('ref_axis',(1.,0.,0.));
#8545=DIRECTION('center_axis',(0.,1.,0.));
#8546=DIRECTION('ref_axis',(1.,0.,0.));
#8547=DIRECTION('center_axis',(0.,1.,0.));
#8548=DIRECTION('ref_axis',(1.,0.,0.));
#8549=DIRECTION('center_axis',(0.,1.,0.));
#8550=DIRECTION('ref_axis',(1.,0.,0.));
#8551=DIRECTION('center_axis',(0.,1.,0.));
#8552=DIRECTION('ref_axis',(1.,0.,0.));
#8553=DIRECTION('center_axis',(0.,1.,0.));
#8554=DIRECTION('ref_axis',(1.,0.,0.));
#8555=DIRECTION('center_axis',(0.,1.,0.));
#8556=DIRECTION('ref_axis',(1.,0.,0.));
#8557=DIRECTION('center_axis',(0.,1.,0.));
#8558=DIRECTION('ref_axis',(1.,0.,0.));
#8559=DIRECTION('center_axis',(0.,1.,0.));
#8560=DIRECTION('ref_axis',(1.,0.,0.));
#8561=DIRECTION('center_axis',(0.,1.,0.));
#8562=DIRECTION('ref_axis',(1.,0.,0.));
#8563=DIRECTION('center_axis',(0.,1.,0.));
#8564=DIRECTION('ref_axis',(1.,0.,0.));
#8565=DIRECTION('center_axis',(0.,1.,0.));
#8566=DIRECTION('ref_axis',(1.,0.,0.));
#8567=DIRECTION('center_axis',(0.,1.,0.));
#8568=DIRECTION('ref_axis',(1.,0.,0.));
#8569=DIRECTION('center_axis',(0.,1.,0.));
#8570=DIRECTION('ref_axis',(1.,0.,0.));
#8571=DIRECTION('center_axis',(0.,1.,0.));
#8572=DIRECTION('ref_axis',(1.,0.,0.));
#8573=DIRECTION('',(-0.923879532511287,0.,-0.38268343236509));
#8574=DIRECTION('',(0.336889853392221,0.,-0.941544065183021));
#8575=DIRECTION('',(0.242980179903264,0.,-0.970031253194544));
#8576=DIRECTION('',(0.146730474455362,0.,-0.989176509964781));
#8577=DIRECTION('',(0.0490676743274181,0.,-0.998795456205172));
#8578=DIRECTION('',(-0.0490676743274181,0.,-0.998795456205172));
#8579=DIRECTION('',(-0.146730474455362,0.,-0.989176509964781));
#8580=DIRECTION('',(-0.242980179903264,0.,-0.970031253194544));
#8581=DIRECTION('',(-0.336889853392221,0.,-0.941544065183021));
#8582=DIRECTION('',(0.923879532511287,0.,-0.38268343236509));
#8583=DIRECTION('center_axis',(0.,1.,0.));
#8584=DIRECTION('ref_axis',(1.,0.,0.));
#8585=DIRECTION('',(0.130526192220051,0.,0.99144486137381));
#8586=DIRECTION('',(-0.983846005927078,0.,0.179016861276632));
#8587=DIRECTION('',(-0.961561797682962,0.,0.274588618184932));
#8588=DIRECTION('',(-0.930017223684012,0.,0.367515936594703));
#8589=DIRECTION('',(-0.889516075421856,0.,0.45690387563042));
#8590=DIRECTION('',(-0.840448401094438,0.,0.541891580574752));
#8591=DIRECTION('',(-0.78328674922865,0.,0.621660573370077));
#8592=DIRECTION('',(-0.718581617779698,0.,0.695442635009612));
#8593=DIRECTION('',(-0.646956152534857,0.,0.762527203906388));
#8594=DIRECTION('',(-0.793353340291235,0.,-0.608761429008721));
#8595=DIRECTION('center_axis',(0.,1.,0.));
#8596=DIRECTION('ref_axis',(1.,0.,0.));
#8597=DIRECTION('center_axis',(0.,1.,0.));
#8598=DIRECTION('ref_axis',(1.,0.,0.));
#8599=DIRECTION('center_axis',(-0.179016861276632,0.,-0.983846005927078));
#8600=DIRECTION('ref_axis',(0.983846005927078,0.,-0.179016861276632));
#8601=DIRECTION('',(-0.983846005927078,0.,0.179016861276632));
#8602=DIRECTION('',(0.,-1.,0.));
#8603=DIRECTION('',(0.983846005927078,0.,-0.179016861276632));
#8604=DIRECTION('',(0.,-1.,0.));
#8605=DIRECTION('center_axis',(-0.274588618184931,0.,-0.961561797682962));
#8606=DIRECTION('ref_axis',(0.961561797682962,0.,-0.274588618184931));
#8607=DIRECTION('',(-0.961561797682962,0.,0.274588618184931));
#8608=DIRECTION('',(0.961561797682962,0.,-0.274588618184931));
#8609=DIRECTION('',(0.,-1.,0.));
#8610=DIRECTION('center_axis',(-0.367515936594702,0.,-0.930017223684013));
#8611=DIRECTION('ref_axis',(0.930017223684013,0.,-0.367515936594702));
#8612=DIRECTION('',(-0.930017223684013,0.,0.367515936594703));
#8613=DIRECTION('',(0.930017223684013,0.,-0.367515936594702));
#8614=DIRECTION('',(0.,-1.,0.));
#8615=DIRECTION('center_axis',(-0.456903875630422,0.,-0.889516075421855));
#8616=DIRECTION('ref_axis',(0.889516075421855,0.,-0.456903875630422));
#8617=DIRECTION('',(-0.889516075421855,0.,0.456903875630422));
#8618=DIRECTION('',(0.889516075421855,0.,-0.456903875630422));
#8619=DIRECTION('',(0.,-1.,0.));
#8620=DIRECTION('center_axis',(-0.54189158057475,0.,-0.840448401094439));
#8621=DIRECTION('ref_axis',(0.840448401094439,0.,-0.54189158057475));
#8622=DIRECTION('',(-0.840448401094439,0.,0.54189158057475));
#8623=DIRECTION('',(0.840448401094439,0.,-0.54189158057475));
#8624=DIRECTION('',(0.,-1.,0.));
#8625=DIRECTION('center_axis',(-0.621660573370078,0.,-0.78328674922865));
#8626=DIRECTION('ref_axis',(0.78328674922865,0.,-0.621660573370078));
#8627=DIRECTION('',(-0.78328674922865,0.,0.621660573370078));
#8628=DIRECTION('',(0.78328674922865,0.,-0.621660573370078));
#8629=DIRECTION('',(0.,-1.,0.));
#8630=DIRECTION('center_axis',(-0.695442635009612,0.,-0.718581617779698));
#8631=DIRECTION('ref_axis',(0.718581617779698,0.,-0.695442635009612));
#8632=DIRECTION('',(-0.718581617779698,0.,0.695442635009612));
#8633=DIRECTION('',(0.718581617779698,0.,-0.695442635009612));
#8634=DIRECTION('',(0.,-1.,0.));
#8635=DIRECTION('center_axis',(-0.762527203906389,0.,-0.646956152534857));
#8636=DIRECTION('ref_axis',(0.646956152534857,0.,-0.762527203906389));
#8637=DIRECTION('',(-0.646956152534857,0.,0.762527203906389));
#8638=DIRECTION('',(0.646956152534857,0.,-0.762527203906389));
#8639=DIRECTION('',(0.,-1.,0.));
#8640=DIRECTION('center_axis',(-0.608761429008721,0.,0.793353340291235));
#8641=DIRECTION('ref_axis',(-0.793353340291235,0.,-0.608761429008721));
#8642=DIRECTION('',(0.793353340291235,0.,0.608761429008721));
#8643=DIRECTION('',(0.,-1.,0.));
#8644=DIRECTION('center_axis',(0.762527203906388,0.,0.646956152534857));
#8645=DIRECTION('ref_axis',(-0.646956152534857,0.,0.762527203906388));
#8646=DIRECTION('',(0.646956152534857,0.,-0.762527203906388));
#8647=DIRECTION('',(0.,-1.,0.));
#8648=DIRECTION('center_axis',(0.695442635009612,0.,0.718581617779698));
#8649=DIRECTION('ref_axis',(-0.718581617779698,0.,0.695442635009612));
#8650=DIRECTION('',(0.718581617779698,0.,-0.695442635009612));
#8651=DIRECTION('',(0.,-1.,0.));
#8652=DIRECTION('center_axis',(0.621660573370077,0.,0.78328674922865));
#8653=DIRECTION('ref_axis',(-0.78328674922865,0.,0.621660573370077));
#8654=DIRECTION('',(0.78328674922865,0.,-0.621660573370077));
#8655=DIRECTION('',(0.,-1.,0.));
#8656=DIRECTION('center_axis',(0.541891580574752,0.,0.840448401094438));
#8657=DIRECTION('ref_axis',(-0.840448401094438,0.,0.541891580574752));
#8658=DIRECTION('',(0.840448401094438,0.,-0.541891580574752));
#8659=DIRECTION('',(0.,-1.,0.));
#8660=DIRECTION('center_axis',(0.45690387563042,0.,0.889516075421856));
#8661=DIRECTION('ref_axis',(-0.889516075421856,0.,0.45690387563042));
#8662=DIRECTION('',(0.889516075421856,0.,-0.45690387563042));
#8663=DIRECTION('',(0.,-1.,0.));
#8664=DIRECTION('center_axis',(0.367515936594703,0.,0.930017223684012));
#8665=DIRECTION('ref_axis',(-0.930017223684012,0.,0.367515936594703));
#8666=DIRECTION('',(0.930017223684012,0.,-0.367515936594703));
#8667=DIRECTION('',(0.,-1.,0.));
#8668=DIRECTION('center_axis',(0.274588618184932,0.,0.961561797682962));
#8669=DIRECTION('ref_axis',(-0.961561797682962,0.,0.274588618184932));
#8670=DIRECTION('',(0.961561797682962,0.,-0.274588618184932));
#8671=DIRECTION('',(0.,-1.,0.));
#8672=DIRECTION('center_axis',(0.179016861276632,0.,0.983846005927078));
#8673=DIRECTION('ref_axis',(-0.983846005927078,0.,0.179016861276632));
#8674=DIRECTION('',(0.983846005927078,0.,-0.179016861276632));
#8675=DIRECTION('',(0.,-1.,0.));
#8676=DIRECTION('center_axis',(0.99144486137381,0.,-0.130526192220051));
#8677=DIRECTION('ref_axis',(0.130526192220051,0.,0.99144486137381));
#8678=DIRECTION('',(-0.130526192220051,0.,-0.99144486137381));
#8679=DIRECTION('center_axis',(0.,1.,0.));
#8680=DIRECTION('ref_axis',(-0.5,0.,-0.866025403784439));
#8681=DIRECTION('center_axis',(0.,1.,0.));
#8682=DIRECTION('ref_axis',(1.,0.,0.));
#8683=DIRECTION('center_axis',(0.,1.,0.));
#8684=DIRECTION('ref_axis',(1.,0.,0.));
#8685=DIRECTION('center_axis',(0.,1.,0.));
#8686=DIRECTION('ref_axis',(1.,0.,0.));
#8687=DIRECTION('center_axis',(0.,1.,0.));
#8688=DIRECTION('ref_axis',(1.,0.,0.));
#8689=DIRECTION('center_axis',(0.,1.,0.));
#8690=DIRECTION('ref_axis',(1.,0.,0.));
#8691=DIRECTION('center_axis',(0.,1.,0.));
#8692=DIRECTION('ref_axis',(1.,0.,0.));
#8693=DIRECTION('center_axis',(0.,1.,0.));
#8694=DIRECTION('ref_axis',(1.,0.,0.));
#8695=DIRECTION('center_axis',(0.,1.,0.));
#8696=DIRECTION('ref_axis',(1.,0.,0.));
#8697=DIRECTION('center_axis',(0.,1.,0.));
#8698=DIRECTION('ref_axis',(1.,0.,0.));
#8699=DIRECTION('center_axis',(0.,1.,0.));
#8700=DIRECTION('ref_axis',(1.,0.,0.));
#8701=DIRECTION('center_axis',(0.,1.,0.));
#8702=DIRECTION('ref_axis',(1.,0.,0.));
#8703=DIRECTION('center_axis',(0.,1.,0.));
#8704=DIRECTION('ref_axis',(1.,0.,0.));
#8705=DIRECTION('center_axis',(0.,1.,0.));
#8706=DIRECTION('ref_axis',(1.,0.,0.));
#8707=DIRECTION('center_axis',(0.,1.,0.));
#8708=DIRECTION('ref_axis',(1.,0.,0.));
#8709=DIRECTION('center_axis',(0.,1.,0.));
#8710=DIRECTION('ref_axis',(1.,0.,0.));
#8711=DIRECTION('center_axis',(0.,1.,0.));
#8712=DIRECTION('ref_axis',(1.,0.,0.));
#8713=DIRECTION('center_axis',(0.94154406518302,0.,0.336889853392221));
#8714=DIRECTION('ref_axis',(-0.336889853392221,0.,0.94154406518302));
#8715=DIRECTION('',(0.336889853392221,0.,-0.94154406518302));
#8716=DIRECTION('',(0.,-1.,0.));
#8717=DIRECTION('',(-0.336889853392221,0.,0.94154406518302));
#8718=DIRECTION('',(0.,-1.,0.));
#8719=DIRECTION('center_axis',(0.970031253194544,0.,0.242980179903265));
#8720=DIRECTION('ref_axis',(-0.242980179903265,0.,0.970031253194544));
#8721=DIRECTION('',(0.242980179903265,0.,-0.970031253194544));
#8722=DIRECTION('',(-0.242980179903265,0.,0.970031253194544));
#8723=DIRECTION('',(0.,-1.,0.));
#8724=DIRECTION('center_axis',(0.989176509964781,0.,0.146730474455363));
#8725=DIRECTION('ref_axis',(-0.146730474455363,0.,0.989176509964781));
#8726=DIRECTION('',(0.146730474455363,0.,-0.989176509964781));
#8727=DIRECTION('',(-0.146730474455363,0.,0.989176509964781));
#8728=DIRECTION('',(0.,-1.,0.));
#8729=DIRECTION('center_axis',(0.998795456205173,0.,0.049067674327416));
#8730=DIRECTION('ref_axis',(-0.049067674327416,0.,0.998795456205173));
#8731=DIRECTION('',(0.049067674327416,0.,-0.998795456205173));
#8732=DIRECTION('',(-0.049067674327416,0.,0.998795456205173));
#8733=DIRECTION('',(0.,-1.,0.));
#8734=DIRECTION('center_axis',(0.998795456205173,0.,-0.049067674327416));
#8735=DIRECTION('ref_axis',(0.049067674327416,0.,0.998795456205173));
#8736=DIRECTION('',(-0.049067674327416,0.,-0.998795456205173));
#8737=DIRECTION('',(0.049067674327416,0.,0.998795456205173));
#8738=DIRECTION('',(0.,-1.,0.));
#8739=DIRECTION('center_axis',(0.989176509964781,0.,-0.146730474455363));
#8740=DIRECTION('ref_axis',(0.146730474455363,0.,0.989176509964781));
#8741=DIRECTION('',(-0.146730474455363,0.,-0.989176509964781));
#8742=DIRECTION('',(0.146730474455363,0.,0.989176509964781));
#8743=DIRECTION('',(0.,-1.,0.));
#8744=DIRECTION('center_axis',(0.970031253194544,0.,-0.242980179903265));
#8745=DIRECTION('ref_axis',(0.242980179903265,0.,0.970031253194544));
#8746=DIRECTION('',(-0.242980179903265,0.,-0.970031253194544));
#8747=DIRECTION('',(0.242980179903265,0.,0.970031253194544));
#8748=DIRECTION('',(0.,-1.,0.));
#8749=DIRECTION('center_axis',(0.94154406518302,0.,-0.336889853392221));
#8750=DIRECTION('ref_axis',(0.336889853392221,0.,0.94154406518302));
#8751=DIRECTION('',(-0.336889853392221,0.,-0.94154406518302));
#8752=DIRECTION('',(0.336889853392221,0.,0.94154406518302));
#8753=DIRECTION('',(0.,-1.,0.));
#8754=DIRECTION('center_axis',(-0.38268343236509,0.,-0.923879532511287));
#8755=DIRECTION('ref_axis',(0.923879532511287,0.,-0.38268343236509));
#8756=DIRECTION('',(-0.923879532511287,0.,0.38268343236509));
#8757=DIRECTION('',(0.,-1.,0.));
#8758=DIRECTION('center_axis',(-0.941544065183021,0.,0.336889853392221));
#8759=DIRECTION('ref_axis',(-0.336889853392221,0.,-0.941544065183021));
#8760=DIRECTION('',(0.336889853392221,0.,0.941544065183021));
#8761=DIRECTION('',(0.,-1.,0.));
#8762=DIRECTION('center_axis',(-0.970031253194544,0.,0.242980179903264));
#8763=DIRECTION('ref_axis',(-0.242980179903264,0.,-0.970031253194544));
#8764=DIRECTION('',(0.242980179903264,0.,0.970031253194544));
#8765=DIRECTION('',(0.,-1.,0.));
#8766=DIRECTION('center_axis',(-0.989176509964781,0.,0.146730474455362));
#8767=DIRECTION('ref_axis',(-0.146730474455362,0.,-0.989176509964781));
#8768=DIRECTION('',(0.146730474455362,0.,0.989176509964781));
#8769=DIRECTION('',(0.,-1.,0.));
#8770=DIRECTION('center_axis',(-0.998795456205172,0.,0.0490676743274181));
#8771=DIRECTION('ref_axis',(-0.0490676743274181,0.,-0.998795456205172));
#8772=DIRECTION('',(0.0490676743274181,0.,0.998795456205172));
#8773=DIRECTION('',(0.,-1.,0.));
#8774=DIRECTION('center_axis',(-0.998795456205172,0.,-0.0490676743274181));
#8775=DIRECTION('ref_axis',(0.0490676743274181,0.,-0.998795456205172));
#8776=DIRECTION('',(-0.0490676743274181,0.,0.998795456205172));
#8777=DIRECTION('',(0.,-1.,0.));
#8778=DIRECTION('center_axis',(-0.989176509964781,0.,-0.146730474455362));
#8779=DIRECTION('ref_axis',(0.146730474455362,0.,-0.989176509964781));
#8780=DIRECTION('',(-0.146730474455362,0.,0.989176509964781));
#8781=DIRECTION('',(0.,-1.,0.));
#8782=DIRECTION('center_axis',(-0.970031253194544,0.,-0.242980179903264));
#8783=DIRECTION('ref_axis',(0.242980179903264,0.,-0.970031253194544));
#8784=DIRECTION('',(-0.242980179903264,0.,0.970031253194544));
#8785=DIRECTION('',(0.,-1.,0.));
#8786=DIRECTION('center_axis',(-0.941544065183021,0.,-0.336889853392221));
#8787=DIRECTION('ref_axis',(0.336889853392221,0.,-0.941544065183021));
#8788=DIRECTION('',(-0.336889853392221,0.,0.941544065183021));
#8789=DIRECTION('',(0.,-1.,0.));
#8790=DIRECTION('center_axis',(-0.38268343236509,0.,0.923879532511287));
#8791=DIRECTION('ref_axis',(-0.923879532511287,0.,-0.38268343236509));
#8792=DIRECTION('',(0.923879532511287,0.,0.38268343236509));
#8793=DIRECTION('center_axis',(0.,1.,0.));
#8794=DIRECTION('ref_axis',(1.,0.,0.));
#8795=DIRECTION('center_axis',(0.,1.,0.));
#8796=DIRECTION('ref_axis',(1.,0.,0.));
#8797=DIRECTION('center_axis',(0.,1.,0.));
#8798=DIRECTION('ref_axis',(1.,0.,0.));
#8799=DIRECTION('center_axis',(0.,1.,0.));
#8800=DIRECTION('ref_axis',(1.,0.,0.));
#8801=DIRECTION('center_axis',(0.,1.,0.));
#8802=DIRECTION('ref_axis',(1.,0.,0.));
#8803=DIRECTION('center_axis',(0.,1.,0.));
#8804=DIRECTION('ref_axis',(1.,0.,0.));
#8805=DIRECTION('center_axis',(0.,1.,0.));
#8806=DIRECTION('ref_axis',(1.,0.,0.));
#8807=DIRECTION('center_axis',(0.,1.,0.));
#8808=DIRECTION('ref_axis',(1.,0.,0.));
#8809=DIRECTION('center_axis',(0.,1.,0.));
#8810=DIRECTION('ref_axis',(1.,0.,0.));
#8811=DIRECTION('center_axis',(0.,1.,0.));
#8812=DIRECTION('ref_axis',(1.,0.,0.));
#8813=DIRECTION('center_axis',(0.,1.,0.));
#8814=DIRECTION('ref_axis',(1.,0.,0.));
#8815=DIRECTION('center_axis',(0.,1.,0.));
#8816=DIRECTION('ref_axis',(1.,0.,0.));
#8817=DIRECTION('center_axis',(0.,1.,0.));
#8818=DIRECTION('ref_axis',(1.,0.,0.));
#8819=DIRECTION('center_axis',(0.,1.,0.));
#8820=DIRECTION('ref_axis',(1.,0.,0.));
#8821=DIRECTION('center_axis',(0.,1.,0.));
#8822=DIRECTION('ref_axis',(1.,0.,0.));
#8823=DIRECTION('center_axis',(0.,1.,0.));
#8824=DIRECTION('ref_axis',(1.,0.,0.));
#8825=DIRECTION('center_axis',(0.,1.,0.));
#8826=DIRECTION('ref_axis',(1.,0.,0.));
#8827=DIRECTION('center_axis',(0.,-1.,0.));
#8828=DIRECTION('ref_axis',(1.,0.,0.));
#8829=DIRECTION('center_axis',(0.,-1.,0.));
#8830=DIRECTION('ref_axis',(1.,0.,0.));
#8831=DIRECTION('',(0.,1.,0.));
#8832=DIRECTION('center_axis',(0.,1.,0.));
#8833=DIRECTION('ref_axis',(1.,0.,0.));
#10471=CARTESIAN_POINT('',(0.,0.,0.));
#10472=CARTESIAN_POINT('Origin',(0.,-1.525,0.));
#10473=CARTESIAN_POINT('',(0.21,-1.525,0.562049819855856));
#10474=CARTESIAN_POINT('',(-0.21,-1.525,0.562049819855856));
#10475=CARTESIAN_POINT('Ctrl Pts',(0.21,-1.525,0.562049819855856));
#10476=CARTESIAN_POINT('Ctrl Pts',(0.21,-1.49837871751922,0.562049819855856));
#10477=CARTESIAN_POINT('Ctrl Pts',(0.204633348688358,-1.4701551027118,0.564140225270058));
#10478=CARTESIAN_POINT('Ctrl Pts',(0.183136586201564,-1.41849286725608,
0.571480520223595));
#10479=CARTESIAN_POINT('Ctrl Pts',(0.167016776838808,-1.39503192874046,
0.576602928616412));
#10480=CARTESIAN_POINT('Ctrl Pts',(0.129978636309075,-1.35799378821073,
0.586063715219224));
#10481=CARTESIAN_POINT('Ctrl Pts',(0.106513536936886,-1.34186587223919,
0.591045521796147));
#10482=CARTESIAN_POINT('Ctrl Pts',(0.0548356965671431,-1.32036302924048,
0.598057680137));
#10483=CARTESIAN_POINT('Ctrl Pts',(0.0266060994851219,-1.315,0.6));
#10484=CARTESIAN_POINT('Ctrl Pts',(-0.026606099485122,-1.315,0.6));
#10485=CARTESIAN_POINT('Ctrl Pts',(-0.0548356965671431,-1.32036302924048,
0.598057680137));
#10486=CARTESIAN_POINT('Ctrl Pts',(-0.106513536936886,-1.34186587223919,
0.591045521796147));
#10487=CARTESIAN_POINT('Ctrl Pts',(-0.129978636309075,-1.35799378821073,
0.586063715219224));
#10488=CARTESIAN_POINT('Ctrl Pts',(-0.167016776838808,-1.39503192874046,
0.576602928616412));
#10489=CARTESIAN_POINT('Ctrl Pts',(-0.183136586201564,-1.41849286725608,
0.571480520223595));
#10490=CARTESIAN_POINT('Ctrl Pts',(-0.204633348688358,-1.4701551027118,
0.564140225270058));
#10491=CARTESIAN_POINT('Ctrl Pts',(-0.21,-1.49837871751922,0.562049819855856));
#10492=CARTESIAN_POINT('Ctrl Pts',(-0.21,-1.525,0.562049819855856));
#10493=CARTESIAN_POINT('Ctrl Pts',(-0.21,-1.525,0.562049819855856));
#10494=CARTESIAN_POINT('Ctrl Pts',(-0.21,-1.55162128248078,0.562049819855856));
#10495=CARTESIAN_POINT('Ctrl Pts',(-0.204633348688358,-1.5798448972882,
0.564140225270058));
#10496=CARTESIAN_POINT('Ctrl Pts',(-0.183136586201564,-1.63150713274392,
0.571480520223595));
#10497=CARTESIAN_POINT('Ctrl Pts',(-0.167016776838808,-1.65496807125954,
0.576602928616412));
#10498=CARTESIAN_POINT('Ctrl Pts',(-0.129978636309075,-1.69200621178927,
0.586063715219224));
#10499=CARTESIAN_POINT('Ctrl Pts',(-0.106513536936886,-1.70813412776081,
0.591045521796147));
#10500=CARTESIAN_POINT('Ctrl Pts',(-0.0548356965671429,-1.72963697075952,
0.598057680137));
#10501=CARTESIAN_POINT('Ctrl Pts',(-0.026606099485122,-1.735,0.6));
#10502=CARTESIAN_POINT('Ctrl Pts',(0.026606099485122,-1.735,0.6));
#10503=CARTESIAN_POINT('Ctrl Pts',(0.0548356965671429,-1.72963697075952,
0.598057680137));
#10504=CARTESIAN_POINT('Ctrl Pts',(0.106513536936886,-1.70813412776081,
0.591045521796147));
#10505=CARTESIAN_POINT('Ctrl Pts',(0.129978636309075,-1.69200621178927,
0.586063715219224));
#10506=CARTESIAN_POINT('Ctrl Pts',(0.167016776838808,-1.65496807125954,
0.576602928616412));
#10507=CARTESIAN_POINT('Ctrl Pts',(0.183136586201564,-1.63150713274392,
0.571480520223595));
#10508=CARTESIAN_POINT('Ctrl Pts',(0.204633348688358,-1.5798448972882,0.564140225270058));
#10509=CARTESIAN_POINT('Ctrl Pts',(0.21,-1.55162128248078,0.562049819855856));
#10510=CARTESIAN_POINT('Ctrl Pts',(0.21,-1.525,0.562049819855856));
#10511=CARTESIAN_POINT('',(-0.21,-1.525,1.35380944006164));
#10512=CARTESIAN_POINT('',(-0.21,-1.525,0.));
#10513=CARTESIAN_POINT('Ctrl Pts',(-0.21,-1.525,1.35380944006164));
#10514=CARTESIAN_POINT('Ctrl Pts',(-0.21,-1.49858689919462,1.35380944006164));
#10515=CARTESIAN_POINT('Ctrl Pts',(-0.204712795751841,-1.47044219200607,
1.35466231450937));
#10516=CARTESIAN_POINT('Ctrl Pts',(-0.183268700413686,-1.41871515620915,
1.35772968493193));
#10517=CARTESIAN_POINT('Ctrl Pts',(-0.167114046419118,-1.39512919832077,
1.35989844568037));
#10518=CARTESIAN_POINT('Ctrl Pts',(-0.129871156089225,-1.35788630799087,
1.36395907436197));
#10519=CARTESIAN_POINT('Ctrl Pts',(-0.106285045427176,-1.34173137598416,
1.36611666311719));
#10520=CARTESIAN_POINT('Ctrl Pts',(-0.0545574871667227,-1.32028707843824,
1.36915840160825));
#10521=CARTESIAN_POINT('Ctrl Pts',(-0.026412598106597,-1.315,1.37));
#10522=CARTESIAN_POINT('Ctrl Pts',(0.0264125981065971,-1.315,1.37));
#10523=CARTESIAN_POINT('Ctrl Pts',(0.0545574871667228,-1.32028707843824,
1.36915840160825));
#10524=CARTESIAN_POINT('Ctrl Pts',(0.106285045427176,-1.34173137598416,
1.36611666311719));
#10525=CARTESIAN_POINT('Ctrl Pts',(0.129871156089225,-1.35788630799087,
1.36395907436197));
#10526=CARTESIAN_POINT('Ctrl Pts',(0.167114046419118,-1.39512919832077,
1.35989844568037));
#10527=CARTESIAN_POINT('Ctrl Pts',(0.183268700413687,-1.41871515620915,
1.35772968493193));
#10528=CARTESIAN_POINT('Ctrl Pts',(0.204712795751841,-1.47044219200607,
1.35466231450937));
#10529=CARTESIAN_POINT('Ctrl Pts',(0.21,-1.49858689919462,1.35380944006164));
#10530=CARTESIAN_POINT('Ctrl Pts',(0.21,-1.55141310080538,1.35380944006164));
#10531=CARTESIAN_POINT('Ctrl Pts',(0.204712795751841,-1.57955780799393,
1.35466231450937));
#10532=CARTESIAN_POINT('Ctrl Pts',(0.183268700413686,-1.63128484379085,
1.35772968493193));
#10533=CARTESIAN_POINT('Ctrl Pts',(0.167114046419118,-1.65487080167923,
1.35989844568037));
#10534=CARTESIAN_POINT('Ctrl Pts',(0.129871156089225,-1.69211369200913,
1.36395907436197));
#10535=CARTESIAN_POINT('Ctrl Pts',(0.106285045427176,-1.70826862401584,
1.36611666311719));
#10536=CARTESIAN_POINT('Ctrl Pts',(0.0545574871667227,-1.72971292156176,
1.36915840160825));
#10537=CARTESIAN_POINT('Ctrl Pts',(0.0264125981065971,-1.735,1.37));
#10538=CARTESIAN_POINT('Ctrl Pts',(-0.026412598106597,-1.735,1.37));
#10539=CARTESIAN_POINT('Ctrl Pts',(-0.0545574871667227,-1.72971292156176,
1.36915840160825));
#10540=CARTESIAN_POINT('Ctrl Pts',(-0.106285045427176,-1.70826862401584,
1.36611666311719));
#10541=CARTESIAN_POINT('Ctrl Pts',(-0.129871156089225,-1.69211369200912,
1.36395907436197));
#10542=CARTESIAN_POINT('Ctrl Pts',(-0.167114046419118,-1.65487080167923,
1.35989844568037));
#10543=CARTESIAN_POINT('Ctrl Pts',(-0.183268700413686,-1.63128484379085,
1.35772968493193));
#10544=CARTESIAN_POINT('Ctrl Pts',(-0.204712795751841,-1.57955780799393,
1.35466231450937));
#10545=CARTESIAN_POINT('Ctrl Pts',(-0.21,-1.55141310080538,1.35380944006164));
#10546=CARTESIAN_POINT('Ctrl Pts',(-0.21,-1.525,1.35380944006164));
#10547=CARTESIAN_POINT('Origin',(0.,0.,0.));
#10548=CARTESIAN_POINT('',(-0.6,-2.05,7.34788079488412E-17));
#10549=CARTESIAN_POINT('Origin',(0.,-2.05,0.));
#10550=CARTESIAN_POINT('',(-0.6,-1.,-7.34788079488412E-17));
#10551=CARTESIAN_POINT('',(-0.6,0.,7.34788079488412E-17));
#10552=CARTESIAN_POINT('Origin',(0.,-1.,0.));
#10553=CARTESIAN_POINT('Origin',(-0.999913779596035,-0.4,0.936521453771333));
#10554=CARTESIAN_POINT('',(-1.08689407619899,-0.4,0.834003157741947));
#10555=CARTESIAN_POINT('',(-0.999913779596035,-0.4,0.936521453771333));
#10556=CARTESIAN_POINT('',(-1.08689407619899,-0.4,0.834003157741947));
#10557=CARTESIAN_POINT('',(-1.08689407619899,-1.,0.834003157741947));
#10558=CARTESIAN_POINT('',(-1.08689407619899,-0.4,0.834003157741947));
#10559=CARTESIAN_POINT('',(-0.999913779596035,-1.,0.936521453771333));
#10560=CARTESIAN_POINT('',(-1.02165885374678,-1.,0.910891879763986));
#10561=CARTESIAN_POINT('',(-0.999913779596035,-0.4,0.936521453771333));
#10562=CARTESIAN_POINT('Origin',(-0.903303766687095,-0.4,1.0300205362462));
#10563=CARTESIAN_POINT('',(-0.903303766687095,-0.4,1.0300205362462));
#10564=CARTESIAN_POINT('',(-0.999913779596035,-0.4,0.936521453771333));
#10565=CARTESIAN_POINT('',(-0.903303766687095,-1.,1.0300205362462));
#10566=CARTESIAN_POINT('',(-0.92745626991433,-1.,1.00664576562748));
#10567=CARTESIAN_POINT('',(-0.903303766687095,-0.4,1.0300205362462));
#10568=CARTESIAN_POINT('Origin',(-0.79799444470889,-0.4,1.11359995789051));
#10569=CARTESIAN_POINT('',(-0.79799444470889,-0.4,1.11359995789051));
#10570=CARTESIAN_POINT('',(-0.903303766687095,-0.4,1.0300205362462));
#10571=CARTESIAN_POINT('',(-0.79799444470889,-1.,1.11359995789051));
#10572=CARTESIAN_POINT('',(-0.824321775203442,-1.,1.09270510247943));
#10573=CARTESIAN_POINT('',(-0.79799444470889,-0.4,1.11359995789051));
#10574=CARTESIAN_POINT('Origin',(-0.685,-0.4,1.18645480318468));
#10575=CARTESIAN_POINT('',(-0.685,-0.4,1.18645480318468));
#10576=CARTESIAN_POINT('',(-0.79799444470889,-0.4,1.11359995789051));
#10577=CARTESIAN_POINT('',(-0.685,-1.,1.18645480318468));
#10578=CARTESIAN_POINT('',(-0.713248611177222,-1.,1.16824109186114));
#10579=CARTESIAN_POINT('',(-0.685,-0.4,1.18645480318468));
#10580=CARTESIAN_POINT('Origin',(-0.565408630832021,-0.4,1.24788344014201));
#10581=CARTESIAN_POINT('',(-0.565408630832021,-0.4,1.24788344014201));
#10582=CARTESIAN_POINT('',(-0.685,-0.4,1.18645480318468));
#10583=CARTESIAN_POINT('',(-0.565408630832022,-1.,1.24788344014201));
#10584=CARTESIAN_POINT('',(-0.595306473124018,-1.,1.23252628090268));
#10585=CARTESIAN_POINT('',(-0.565408630832021,-0.4,1.24788344014201));
#10586=CARTESIAN_POINT('Origin',(-0.440372067465332,-0.4,1.29729427740829));
#10587=CARTESIAN_POINT('',(-0.440372067465332,-0.4,1.29729427740829));
#10588=CARTESIAN_POINT('',(-0.565408630832021,-0.4,1.24788344014201));
#10589=CARTESIAN_POINT('',(-0.440372067465332,-1.,1.29729427740829));
#10590=CARTESIAN_POINT('',(-0.471631208307004,-1.,1.28494156809172));
#10591=CARTESIAN_POINT('',(-0.440372067465332,-0.4,1.29729427740829));
#10592=CARTESIAN_POINT('Origin',(-0.311094480357092,-0.4,1.33421146160995));
#10593=CARTESIAN_POINT('',(-0.311094480357092,-0.4,1.33421146160995));
#10594=CARTESIAN_POINT('',(-0.440372067465332,-0.4,1.29729427740829));
#10595=CARTESIAN_POINT('',(-0.311094480357092,-1.,1.33421146160995));
#10596=CARTESIAN_POINT('',(-0.343413877134152,-1.,1.32498216555953));
#10597=CARTESIAN_POINT('',(-0.311094480357092,-0.4,1.33421146160995));
#10598=CARTESIAN_POINT('Origin',(-0.178820883341471,-0.4,1.35827946008212));
#10599=CARTESIAN_POINT('',(-0.178820883341471,-0.4,1.35827946008212));
#10600=CARTESIAN_POINT('',(-0.311094480357092,-0.4,1.33421146160995));
#10601=CARTESIAN_POINT('',(-0.178820883341471,-1.,1.35827946008212));
#10602=CARTESIAN_POINT('',(-0.211889282595376,-1.,1.35226246046408));
#10603=CARTESIAN_POINT('',(-0.178820883341471,-0.4,1.35827946008212));
#10604=CARTESIAN_POINT('Origin',(-0.104420953776042,-0.4,0.793155889099048));
#10605=CARTESIAN_POINT('',(-0.104420953776042,-0.4,0.793155889099048));
#10606=CARTESIAN_POINT('',(-0.178820883341471,-0.4,1.35827946008212));
#10607=CARTESIAN_POINT('',(-0.104420953776042,-1.,0.793155889099048));
#10608=CARTESIAN_POINT('',(-0.0522104768880209,-1.,0.396577944549524));
#10609=CARTESIAN_POINT('',(-0.104420953776042,-0.4,0.793155889099048));
#10610=CARTESIAN_POINT('Origin',(-0.181661010427499,-0.4,0.779101583421867));
#10611=CARTESIAN_POINT('',(-0.181661010427499,-0.4,0.779101583421867));
#10612=CARTESIAN_POINT('',(-0.104420953776042,-0.4,0.793155889099048));
#10613=CARTESIAN_POINT('',(-0.181661010427499,-1.,0.779101583421867));
#10614=CARTESIAN_POINT('',(-0.162350996264634,-1.,0.782615159841162));
#10615=CARTESIAN_POINT('',(-0.181661010427499,-0.4,0.779101583421867));
#10616=CARTESIAN_POINT('Origin',(-0.25715157224253,-0.4,0.757544103596084));
#10617=CARTESIAN_POINT('',(-0.25715157224253,-0.4,0.757544103596084));
#10618=CARTESIAN_POINT('',(-0.181661010427499,-0.4,0.779101583421867));
#10619=CARTESIAN_POINT('',(-0.25715157224253,-1.,0.757544103596084));
#10620=CARTESIAN_POINT('',(-0.238278931788772,-1.,0.76293347355253));
#10621=CARTESIAN_POINT('',(-0.25715157224253,-0.4,0.757544103596084));
#10622=CARTESIAN_POINT('Origin',(-0.330165623843516,-0.4,0.72869105993694));
#10623=CARTESIAN_POINT('',(-0.330165623843516,-0.4,0.72869105993694));
#10624=CARTESIAN_POINT('',(-0.25715157224253,-0.4,0.757544103596084));
#10625=CARTESIAN_POINT('',(-0.330165623843516,-1.,0.72869105993694));
#10626=CARTESIAN_POINT('',(-0.311912110943269,-1.,0.735904320851726));
#10627=CARTESIAN_POINT('',(-0.330165623843516,-0.4,0.72869105993694));
#10628=CARTESIAN_POINT('Origin',(-0.4,-0.4,0.692820323027551));
#10629=CARTESIAN_POINT('',(-0.4,-0.4,0.692820323027551));
#10630=CARTESIAN_POINT('',(-0.330165623843516,-0.4,0.72869105993694));
#10631=CARTESIAN_POINT('',(-0.4,-1.,0.692820323027551));
#10632=CARTESIAN_POINT('',(-0.382541405960879,-1.,0.701788007254898));
#10633=CARTESIAN_POINT('',(-0.4,-0.4,0.692820323027551));
#10634=CARTESIAN_POINT('Origin',(-0.465982157494242,-0.4,0.650277347673292));
#10635=CARTESIAN_POINT('',(-0.465982157494242,-0.4,0.650277347673292));
#10636=CARTESIAN_POINT('',(-0.4,-0.4,0.692820323027551));
#10637=CARTESIAN_POINT('',(-0.465982157494242,-1.,0.650277347673292));
#10638=CARTESIAN_POINT('',(-0.449486618120682,-1.,0.660913091511857));
#10639=CARTESIAN_POINT('',(-0.465982157494242,-0.4,0.650277347673292));
#10640=CARTESIAN_POINT('Origin',(-0.527476652080055,-0.4,0.601471845983182));
#10641=CARTESIAN_POINT('',(-0.527476652080055,-0.4,0.601471845983182));
#10642=CARTESIAN_POINT('',(-0.465982157494242,-0.4,0.650277347673292));
#10643=CARTESIAN_POINT('',(-0.527476652080055,-1.,0.601471845983182));
#10644=CARTESIAN_POINT('',(-0.512103028433602,-1.,0.613673221405709));
#10645=CARTESIAN_POINT('',(-0.527476652080055,-0.4,0.601471845983182));
#10646=CARTESIAN_POINT('Origin',(-0.583891258158269,-0.4,0.546873841618297));
#10647=CARTESIAN_POINT('',(-0.583891258158269,-0.4,0.546873841618297));
#10648=CARTESIAN_POINT('',(-0.527476652080055,-0.4,0.601471845983182));
#10649=CARTESIAN_POINT('',(-0.583891258158269,-1.,0.546873841618297));
#10650=CARTESIAN_POINT('',(-0.569787606638716,-1.,0.560523342709518));
#10651=CARTESIAN_POINT('',(-0.583891258158269,-0.4,0.546873841618297));
#10652=CARTESIAN_POINT('Origin',(-0.634682672232988,-0.4,0.487009143206976));
#10653=CARTESIAN_POINT('',(-0.634682672232988,-0.4,0.487009143206976));
#10654=CARTESIAN_POINT('',(-0.583891258158269,-0.4,0.546873841618297));
#10655=CARTESIAN_POINT('',(-0.634682672232988,-1.,0.487009143206976));
#10656=CARTESIAN_POINT('',(-0.621984818714309,-1.,0.501975317809806));
#10657=CARTESIAN_POINT('',(-0.634682672232988,-0.4,0.487009143206976));
#10658=CARTESIAN_POINT('Origin',(-1.08689407619899,-0.4,0.834003157741947));
#10659=CARTESIAN_POINT('',(-0.634682672232988,-0.4,0.487009143206976));
#10660=CARTESIAN_POINT('',(-0.543447038099496,-1.,0.417001578870973));
#10661=CARTESIAN_POINT('Origin',(-0.527275906502258,-0.4,0.913268659668846));
#10662=CARTESIAN_POINT('Origin',(0.,-1.,0.));
#10663=CARTESIAN_POINT('Origin',(0.,-1.,0.));
#10664=CARTESIAN_POINT('Origin',(0.,-1.,0.));
#10665=CARTESIAN_POINT('Origin',(0.,-1.,0.));
#10666=CARTESIAN_POINT('Origin',(0.,-1.,0.));
#10667=CARTESIAN_POINT('Origin',(0.,-1.,0.));
#10668=CARTESIAN_POINT('Origin',(0.,-1.,0.));
#10669=CARTESIAN_POINT('Origin',(0.,-1.,0.));
#10670=CARTESIAN_POINT('Origin',(0.,-1.,0.));
#10671=CARTESIAN_POINT('Origin',(0.,-1.,0.));
#10672=CARTESIAN_POINT('Origin',(0.,-1.,0.));
#10673=CARTESIAN_POINT('Origin',(0.,-1.,0.));
#10674=CARTESIAN_POINT('Origin',(0.,-1.,0.));
#10675=CARTESIAN_POINT('Origin',(0.,-1.,0.));
#10676=CARTESIAN_POINT('Origin',(0.,-1.,0.));
#10677=CARTESIAN_POINT('Origin',(0.,-1.,0.));
#10678=CARTESIAN_POINT('Origin',(0.,-1.,0.));
#10679=CARTESIAN_POINT('',(1.26571495954046,-1.,0.524276302340173));
#10680=CARTESIAN_POINT('Origin',(0.,-1.,0.));
#10681=CARTESIAN_POINT('',(0.739103626009029,-1.,0.306146745892072));
#10682=CARTESIAN_POINT('',(0.632857479770231,-1.,0.262138151170086));
#10683=CARTESIAN_POINT('',(0.765552268585767,-1.,0.23222774180357));
#10684=CARTESIAN_POINT('',(0.745715786653214,-1.,0.287666994869947));
#10685=CARTESIAN_POINT('',(0.784628224322584,-1.,0.156072257612903));
#10686=CARTESIAN_POINT('',(0.770321257519971,-1.,0.213188870755903));
#10687=CARTESIAN_POINT('',(0.796147781337758,-1.,0.0784137122636485));
#10688=CARTESIAN_POINT('',(0.787508113576378,-1.,0.136657621275589));
#10689=CARTESIAN_POINT('',(0.8,-1.,0.));
#10690=CARTESIAN_POINT('',(0.797110836003318,-1.,0.0588102841977364));
#10691=CARTESIAN_POINT('',(0.796147781337758,-1.,-0.0784137122636485));
#10692=CARTESIAN_POINT('',(0.799036945334439,-1.,-0.0196034280659122));
#10693=CARTESIAN_POINT('',(0.784628224322584,-1.,-0.156072257612903));
#10694=CARTESIAN_POINT('',(0.793267892083964,-1.,-0.0978283486009621));
#10695=CARTESIAN_POINT('',(0.765552268585767,-1.,-0.23222774180357));
#10696=CARTESIAN_POINT('',(0.77985923538838,-1.,-0.17511112866057));
#10697=CARTESIAN_POINT('',(0.739103626009029,-1.,-0.306146745892072));
#10698=CARTESIAN_POINT('',(0.758940107941583,-1.,-0.250707492825696));
#10699=CARTESIAN_POINT('',(1.26571495954046,-1.,-0.524276302340173));
#10700=CARTESIAN_POINT('',(0.369551813004515,-1.,-0.153073372946036));
#10701=CARTESIAN_POINT('',(-0.17882088334147,-1.,-1.35827946008212));
#10702=CARTESIAN_POINT('Origin',(0.,-1.,0.));
#10703=CARTESIAN_POINT('',(-0.104420953776041,-1.,-0.793155889099048));
#10704=CARTESIAN_POINT('',(-0.0894104416707352,-1.,-0.67913973004106));
#10705=CARTESIAN_POINT('',(-0.181661010427498,-1.,-0.779101583421867));
#10706=CARTESIAN_POINT('',(-0.123730967938905,-1.,-0.789642312679753));
#10707=CARTESIAN_POINT('',(-0.257151572242529,-1.,-0.757544103596085));
#10708=CARTESIAN_POINT('',(-0.200533650881256,-1.,-0.773712213465422));
#10709=CARTESIAN_POINT('',(-0.330165623843516,-1.,-0.728691059936941));
#10710=CARTESIAN_POINT('',(-0.275405085142776,-1.,-0.750330842681299));
#10711=CARTESIAN_POINT('',(-0.4,-1.,-0.692820323027551));
#10712=CARTESIAN_POINT('',(-0.347624217882637,-1.,-0.719723375709593));
#10713=CARTESIAN_POINT('',(-0.465982157494242,-1.,-0.650277347673292));
#10714=CARTESIAN_POINT('',(-0.41649553937356,-1.,-0.682184579188986));
#10715=CARTESIAN_POINT('',(-0.527476652080055,-1.,-0.601471845983182));
#10716=CARTESIAN_POINT('',(-0.481355781140695,-1.,-0.638075972250765));
#10717=CARTESIAN_POINT('',(-0.583891258158268,-1.,-0.546873841618297));
#10718=CARTESIAN_POINT('',(-0.541580303599609,-1.,-0.587822344891961));
#10719=CARTESIAN_POINT('',(-0.634682672232988,-1.,-0.487009143206977));
#10720=CARTESIAN_POINT('',(-0.596589111676948,-1.,-0.531907667015467));
#10721=CARTESIAN_POINT('',(-1.08689407619899,-1.,-0.834003157741947));
#10722=CARTESIAN_POINT('',(-0.317341336116494,-1.,-0.243504571603488));
#10723=CARTESIAN_POINT('',(-1.37,-1.,-1.67776611483187E-16));
#10724=CARTESIAN_POINT('Origin',(0.,-1.,0.));
#10725=CARTESIAN_POINT('Origin',(0.,-1.,0.));
#10726=CARTESIAN_POINT('Origin',(-0.311094480357091,-0.4,-1.33421146160995));
#10727=CARTESIAN_POINT('',(-0.17882088334147,-0.4,-1.35827946008212));
#10728=CARTESIAN_POINT('',(-0.311094480357091,-0.4,-1.33421146160995));
#10729=CARTESIAN_POINT('',(-0.17882088334147,-0.4,-1.35827946008212));
#10730=CARTESIAN_POINT('',(-0.17882088334147,-0.4,-1.35827946008212));
#10731=CARTESIAN_POINT('',(-0.311094480357091,-1.,-1.33421146160995));
#10732=CARTESIAN_POINT('',(-0.278026081103185,-1.,-1.34022846122799));
#10733=CARTESIAN_POINT('',(-0.311094480357091,-0.4,-1.33421146160995));
#10734=CARTESIAN_POINT('Origin',(-0.440372067465331,-0.4,-1.29729427740829));
#10735=CARTESIAN_POINT('',(-0.440372067465331,-0.4,-1.29729427740829));
#10736=CARTESIAN_POINT('',(-0.311094480357091,-0.4,-1.33421146160995));
#10737=CARTESIAN_POINT('',(-0.440372067465331,-1.,-1.29729427740829));
#10738=CARTESIAN_POINT('',(-0.408052670688271,-1.,-1.30652357345871));
#10739=CARTESIAN_POINT('',(-0.440372067465331,-0.4,-1.29729427740829));
#10740=CARTESIAN_POINT('Origin',(-0.565408630832021,-0.4,-1.24788344014201));
#10741=CARTESIAN_POINT('',(-0.565408630832021,-0.4,-1.24788344014201));
#10742=CARTESIAN_POINT('',(-0.440372067465331,-0.4,-1.29729427740829));
#10743=CARTESIAN_POINT('',(-0.565408630832021,-1.,-1.24788344014201));
#10744=CARTESIAN_POINT('',(-0.534149489990348,-1.,-1.26023614945858));
#10745=CARTESIAN_POINT('',(-0.565408630832021,-0.4,-1.24788344014201));
#10746=CARTESIAN_POINT('Origin',(-0.685,-0.4,-1.18645480318468));
#10747=CARTESIAN_POINT('',(-0.685,-0.4,-1.18645480318468));
#10748=CARTESIAN_POINT('',(-0.565408630832021,-0.4,-1.24788344014201));
#10749=CARTESIAN_POINT('',(-0.685,-1.,-1.18645480318468));
#10750=CARTESIAN_POINT('',(-0.655102157708006,-1.,-1.20181196242401));
#10751=CARTESIAN_POINT('',(-0.685,-0.4,-1.18645480318468));
#10752=CARTESIAN_POINT('Origin',(-0.797994444708889,-0.4,-1.11359995789051));
#10753=CARTESIAN_POINT('',(-0.797994444708889,-0.4,-1.11359995789051));
#10754=CARTESIAN_POINT('',(-0.685,-0.4,-1.18645480318468));
#10755=CARTESIAN_POINT('',(-0.797994444708889,-1.,-1.11359995789051));
#10756=CARTESIAN_POINT('',(-0.769745833531665,-1.,-1.13181366921406));
#10757=CARTESIAN_POINT('',(-0.797994444708889,-0.4,-1.11359995789051));
#10758=CARTESIAN_POINT('Origin',(-0.903303766687094,-0.4,-1.0300205362462));
#10759=CARTESIAN_POINT('',(-0.903303766687094,-0.4,-1.0300205362462));
#10760=CARTESIAN_POINT('',(-0.797994444708889,-0.4,-1.11359995789051));
#10761=CARTESIAN_POINT('',(-0.903303766687094,-1.,-1.0300205362462));
#10762=CARTESIAN_POINT('',(-0.876976436192543,-1.,-1.05091539165728));
#10763=CARTESIAN_POINT('',(-0.903303766687094,-0.4,-1.0300205362462));
#10764=CARTESIAN_POINT('Origin',(-0.999913779596035,-0.4,-0.936521453771334));
#10765=CARTESIAN_POINT('',(-0.999913779596035,-0.4,-0.936521453771334));
#10766=CARTESIAN_POINT('',(-0.903303766687094,-0.4,-1.0300205362462));
#10767=CARTESIAN_POINT('',(-0.999913779596034,-1.,-0.936521453771334));
#10768=CARTESIAN_POINT('',(-0.9757612763688,-1.,-0.95989622439005));
#10769=CARTESIAN_POINT('',(-0.999913779596035,-0.4,-0.936521453771334));
#10770=CARTESIAN_POINT('Origin',(-1.08689407619899,-0.4,-0.834003157741947));
#10771=CARTESIAN_POINT('',(-1.08689407619899,-0.4,-0.834003157741947));
#10772=CARTESIAN_POINT('',(-0.999913779596035,-0.4,-0.936521453771334));
#10773=CARTESIAN_POINT('',(-1.06514900204825,-1.,-0.859632731749293));
#10774=CARTESIAN_POINT('',(-1.08689407619899,-0.4,-0.834003157741947));
#10775=CARTESIAN_POINT('Origin',(-0.634682672232988,-0.4,-0.487009143206977));
#10776=CARTESIAN_POINT('',(-0.634682672232988,-0.4,-0.487009143206977));
#10777=CARTESIAN_POINT('',(-1.08689407619899,-0.4,-0.834003157741947));
#10778=CARTESIAN_POINT('',(-0.634682672232988,-0.4,-0.487009143206977));
#10779=CARTESIAN_POINT('Origin',(-0.583891258158268,-0.4,-0.546873841618297));
#10780=CARTESIAN_POINT('',(-0.583891258158268,-0.4,-0.546873841618297));
#10781=CARTESIAN_POINT('',(-0.634682672232988,-0.4,-0.487009143206977));
#10782=CARTESIAN_POINT('',(-0.583891258158268,-0.4,-0.546873841618297));
#10783=CARTESIAN_POINT('Origin',(-0.527476652080055,-0.4,-0.601471845983182));
#10784=CARTESIAN_POINT('',(-0.527476652080055,-0.4,-0.601471845983182));
#10785=CARTESIAN_POINT('',(-0.583891258158268,-0.4,-0.546873841618297));
#10786=CARTESIAN_POINT('',(-0.527476652080055,-0.4,-0.601471845983182));
#10787=CARTESIAN_POINT('Origin',(-0.465982157494242,-0.4,-0.650277347673292));
#10788=CARTESIAN_POINT('',(-0.465982157494242,-0.4,-0.650277347673292));
#10789=CARTESIAN_POINT('',(-0.527476652080055,-0.4,-0.601471845983182));
#10790=CARTESIAN_POINT('',(-0.465982157494242,-0.4,-0.650277347673292));
#10791=CARTESIAN_POINT('Origin',(-0.4,-0.4,-0.692820323027551));
#10792=CARTESIAN_POINT('',(-0.4,-0.4,-0.692820323027551));
#10793=CARTESIAN_POINT('',(-0.465982157494242,-0.4,-0.650277347673292));
#10794=CARTESIAN_POINT('',(-0.4,-0.4,-0.692820323027551));
#10795=CARTESIAN_POINT('Origin',(-0.330165623843516,-0.4,-0.728691059936941));
#10796=CARTESIAN_POINT('',(-0.330165623843516,-0.4,-0.728691059936941));
#10797=CARTESIAN_POINT('',(-0.4,-0.4,-0.692820323027551));
#10798=CARTESIAN_POINT('',(-0.330165623843516,-0.4,-0.728691059936941));
#10799=CARTESIAN_POINT('Origin',(-0.257151572242529,-0.4,-0.757544103596085));
#10800=CARTESIAN_POINT('',(-0.257151572242529,-0.4,-0.757544103596085));
#10801=CARTESIAN_POINT('',(-0.330165623843516,-0.4,-0.728691059936941));
#10802=CARTESIAN_POINT('',(-0.257151572242529,-0.4,-0.757544103596085));
#10803=CARTESIAN_POINT('Origin',(-0.181661010427498,-0.4,-0.779101583421867));
#10804=CARTESIAN_POINT('',(-0.181661010427498,-0.4,-0.779101583421867));
#10805=CARTESIAN_POINT('',(-0.257151572242529,-0.4,-0.757544103596085));
#10806=CARTESIAN_POINT('',(-0.181661010427498,-0.4,-0.779101583421867));
#10807=CARTESIAN_POINT('Origin',(-0.104420953776041,-0.4,-0.793155889099048));
#10808=CARTESIAN_POINT('',(-0.104420953776041,-0.4,-0.793155889099048));
#10809=CARTESIAN_POINT('',(-0.181661010427498,-0.4,-0.779101583421867));
#10810=CARTESIAN_POINT('',(-0.104420953776041,-0.4,-0.793155889099048));
#10811=CARTESIAN_POINT('Origin',(-0.17882088334147,-0.4,-1.35827946008212));
#10812=CARTESIAN_POINT('',(-0.104420953776041,-0.4,-0.793155889099048));
#10813=CARTESIAN_POINT('Origin',(-0.527275906502257,-0.4,-0.913268659668847));
#10814=CARTESIAN_POINT('Origin',(0.,-1.,0.));
#10815=CARTESIAN_POINT('Origin',(0.,-1.,0.));
#10816=CARTESIAN_POINT('Origin',(0.,-1.,0.));
#10817=CARTESIAN_POINT('Origin',(0.,-1.,0.));
#10818=CARTESIAN_POINT('Origin',(0.,-1.,0.));
#10819=CARTESIAN_POINT('Origin',(0.,-1.,0.));
#10820=CARTESIAN_POINT('Origin',(0.,-1.,0.));
#10821=CARTESIAN_POINT('Origin',(0.,-1.,0.));
#10822=CARTESIAN_POINT('Origin',(0.,-1.,0.));
#10823=CARTESIAN_POINT('Origin',(0.,-1.,0.));
#10824=CARTESIAN_POINT('Origin',(0.,-1.,0.));
#10825=CARTESIAN_POINT('Origin',(0.,-1.,0.));
#10826=CARTESIAN_POINT('Origin',(0.,-1.,0.));
#10827=CARTESIAN_POINT('Origin',(0.,-1.,0.));
#10828=CARTESIAN_POINT('Origin',(0.,-1.,0.));
#10829=CARTESIAN_POINT('Origin',(0.,-1.,0.));
#10830=CARTESIAN_POINT('Origin',(1.31100825995313,-0.4,0.397690007838613));
#10831=CARTESIAN_POINT('',(1.26571495954046,-0.4,0.524276302340173));
#10832=CARTESIAN_POINT('',(1.31100825995313,-0.4,0.397690007838613));
#10833=CARTESIAN_POINT('',(1.26571495954046,-0.4,0.524276302340173));
#10834=CARTESIAN_POINT('',(1.26571495954046,-0.4,0.524276302340173));
#10835=CARTESIAN_POINT('',(1.31100825995313,-1.,0.397690007838613));
#10836=CARTESIAN_POINT('',(1.29968493484996,-1.,0.429336581464004));
#10837=CARTESIAN_POINT('',(1.31100825995313,-0.4,0.397690007838613));
#10838=CARTESIAN_POINT('Origin',(1.34367583415243,-0.4,0.267273741162096));
#10839=CARTESIAN_POINT('',(1.34367583415243,-0.4,0.267273741162096));
#10840=CARTESIAN_POINT('',(1.31100825995313,-0.4,0.397690007838613));
#10841=CARTESIAN_POINT('',(1.34367583415243,-1.,0.267273741162096));
#10842=CARTESIAN_POINT('',(1.3355089406026,-1.,0.299877807831226));
#10843=CARTESIAN_POINT('',(1.34367583415243,-0.4,0.267273741162096));
#10844=CARTESIAN_POINT('Origin',(1.36340307554091,-0.4,0.134283482251498));
#10845=CARTESIAN_POINT('',(1.36340307554091,-0.4,0.134283482251498));
#10846=CARTESIAN_POINT('',(1.34367583415243,-0.4,0.267273741162096));
#10847=CARTESIAN_POINT('',(1.36340307554091,-1.,0.134283482251498));
#10848=CARTESIAN_POINT('',(1.35847126519379,-1.,0.167531046979148));
#10849=CARTESIAN_POINT('',(1.36340307554091,-0.4,0.134283482251498));
#10850=CARTESIAN_POINT('Origin',(1.37,-0.4,0.));
#10851=CARTESIAN_POINT('',(1.37,-0.4,0.));
#10852=CARTESIAN_POINT('',(1.36340307554091,-0.4,0.134283482251498));
#10853=CARTESIAN_POINT('',(1.37,-1.,0.));
#10854=CARTESIAN_POINT('',(1.36835076888523,-1.,0.0335708705628731));
#10855=CARTESIAN_POINT('',(1.37,-0.4,0.));
#10856=CARTESIAN_POINT('Origin',(1.36340307554091,-0.4,-0.134283482251498));
#10857=CARTESIAN_POINT('',(1.36340307554091,-0.4,-0.134283482251498));
#10858=CARTESIAN_POINT('',(1.37,-0.4,0.));
#10859=CARTESIAN_POINT('',(1.36340307554091,-1.,-0.134283482251498));
#10860=CARTESIAN_POINT('',(1.36505230665568,-1.,-0.100712611688622));
#10861=CARTESIAN_POINT('',(1.36340307554091,-0.4,-0.134283482251498));
#10862=CARTESIAN_POINT('Origin',(1.34367583415243,-0.4,-0.267273741162096));
#10863=CARTESIAN_POINT('',(1.34367583415243,-0.4,-0.267273741162096));
#10864=CARTESIAN_POINT('',(1.36340307554091,-0.4,-0.134283482251498));
#10865=CARTESIAN_POINT('',(1.34367583415243,-1.,-0.267273741162096));
#10866=CARTESIAN_POINT('',(1.34860764449955,-1.,-0.234026176434447));
#10867=CARTESIAN_POINT('',(1.34367583415243,-0.4,-0.267273741162096));
#10868=CARTESIAN_POINT('Origin',(1.31100825995313,-0.4,-0.397690007838613));
#10869=CARTESIAN_POINT('',(1.31100825995313,-0.4,-0.397690007838613));
#10870=CARTESIAN_POINT('',(1.34367583415243,-0.4,-0.267273741162096));
#10871=CARTESIAN_POINT('',(1.31100825995313,-1.,-0.397690007838613));
#10872=CARTESIAN_POINT('',(1.31917515350295,-1.,-0.365085941169485));
#10873=CARTESIAN_POINT('',(1.31100825995313,-0.4,-0.397690007838613));
#10874=CARTESIAN_POINT('Origin',(1.26571495954046,-0.4,-0.524276302340173));
#10875=CARTESIAN_POINT('',(1.26571495954046,-0.4,-0.524276302340173));
#10876=CARTESIAN_POINT('',(1.31100825995313,-0.4,-0.397690007838613));
#10877=CARTESIAN_POINT('',(1.27703828464363,-1.,-0.492629728714784));
#10878=CARTESIAN_POINT('',(1.26571495954046,-0.4,-0.524276302340173));
#10879=CARTESIAN_POINT('Origin',(0.739103626009029,-0.4,-0.306146745892072));
#10880=CARTESIAN_POINT('',(0.739103626009029,-0.4,-0.306146745892072));
#10881=CARTESIAN_POINT('',(1.26571495954046,-0.4,-0.524276302340173));
#10882=CARTESIAN_POINT('',(0.739103626009029,-0.4,-0.306146745892072));
#10883=CARTESIAN_POINT('Origin',(0.765552268585767,-0.4,-0.23222774180357));
#10884=CARTESIAN_POINT('',(0.765552268585767,-0.4,-0.23222774180357));
#10885=CARTESIAN_POINT('',(0.739103626009029,-0.4,-0.306146745892072));
#10886=CARTESIAN_POINT('',(0.765552268585767,-0.4,-0.23222774180357));
#10887=CARTESIAN_POINT('Origin',(0.784628224322584,-0.4,-0.156072257612903));
#10888=CARTESIAN_POINT('',(0.784628224322584,-0.4,-0.156072257612903));
#10889=CARTESIAN_POINT('',(0.765552268585767,-0.4,-0.23222774180357));
#10890=CARTESIAN_POINT('',(0.784628224322584,-0.4,-0.156072257612903));
#10891=CARTESIAN_POINT('Origin',(0.796147781337758,-0.4,-0.0784137122636485));
#10892=CARTESIAN_POINT('',(0.796147781337758,-0.4,-0.0784137122636485));
#10893=CARTESIAN_POINT('',(0.784628224322584,-0.4,-0.156072257612903));
#10894=CARTESIAN_POINT('',(0.796147781337758,-0.4,-0.0784137122636485));
#10895=CARTESIAN_POINT('Origin',(0.8,-0.4,0.));
#10896=CARTESIAN_POINT('',(0.8,-0.4,0.));
#10897=CARTESIAN_POINT('',(0.796147781337758,-0.4,-0.0784137122636485));
#10898=CARTESIAN_POINT('',(0.8,-0.4,0.));
#10899=CARTESIAN_POINT('Origin',(0.796147781337758,-0.4,0.0784137122636485));
#10900=CARTESIAN_POINT('',(0.796147781337758,-0.4,0.0784137122636485));
#10901=CARTESIAN_POINT('',(0.8,-0.4,0.));
#10902=CARTESIAN_POINT('',(0.796147781337758,-0.4,0.0784137122636485));
#10903=CARTESIAN_POINT('Origin',(0.784628224322584,-0.4,0.156072257612903));
#10904=CARTESIAN_POINT('',(0.784628224322584,-0.4,0.156072257612903));
#10905=CARTESIAN_POINT('',(0.796147781337758,-0.4,0.0784137122636485));
#10906=CARTESIAN_POINT('',(0.784628224322584,-0.4,0.156072257612903));
#10907=CARTESIAN_POINT('Origin',(0.765552268585767,-0.4,0.23222774180357));
#10908=CARTESIAN_POINT('',(0.765552268585767,-0.4,0.23222774180357));
#10909=CARTESIAN_POINT('',(0.784628224322584,-0.4,0.156072257612903));
#10910=CARTESIAN_POINT('',(0.765552268585767,-0.4,0.23222774180357));
#10911=CARTESIAN_POINT('Origin',(0.739103626009029,-0.4,0.306146745892072));
#10912=CARTESIAN_POINT('',(0.739103626009029,-0.4,0.306146745892072));
#10913=CARTESIAN_POINT('',(0.765552268585767,-0.4,0.23222774180357));
#10914=CARTESIAN_POINT('',(0.739103626009029,-0.4,0.306146745892072));
#10915=CARTESIAN_POINT('Origin',(1.26571495954046,-0.4,0.524276302340173));
#10916=CARTESIAN_POINT('',(0.739103626009029,-0.4,0.306146745892072));
#10917=CARTESIAN_POINT('Origin',(1.05455181300451,-0.4,0.));
#10918=CARTESIAN_POINT('Origin',(0.,-1.,0.));
#10919=CARTESIAN_POINT('Origin',(0.,-1.,0.));
#10920=CARTESIAN_POINT('Origin',(0.,-1.,0.));
#10921=CARTESIAN_POINT('Origin',(0.,-1.,0.));
#10922=CARTESIAN_POINT('Origin',(0.,-1.,0.));
#10923=CARTESIAN_POINT('Origin',(0.,-1.,0.));
#10924=CARTESIAN_POINT('Origin',(0.,-1.,0.));
#10925=CARTESIAN_POINT('Origin',(0.,-1.,0.));
#10926=CARTESIAN_POINT('Origin',(0.,-1.,0.));
#10927=CARTESIAN_POINT('Origin',(0.,-1.,0.));
#10928=CARTESIAN_POINT('Origin',(0.,-1.,0.));
#10929=CARTESIAN_POINT('Origin',(0.,-1.,0.));
#10930=CARTESIAN_POINT('Origin',(0.,-1.,0.));
#10931=CARTESIAN_POINT('Origin',(0.,-1.,0.));
#10932=CARTESIAN_POINT('Origin',(0.,-1.,0.));
#10933=CARTESIAN_POINT('Origin',(0.,-1.,0.));
#10934=CARTESIAN_POINT('Origin',(0.,-1.,0.));
#10935=CARTESIAN_POINT('',(-1.37,-2.05,1.67776611483187E-16));
#10936=CARTESIAN_POINT('Origin',(0.,-2.05,0.));
#10937=CARTESIAN_POINT('',(-1.37,-1.,-1.67776611483187E-16));
#10938=CARTESIAN_POINT('Origin',(0.,-2.05,0.));
#12325=UNCERTAINTY_MEASURE_WITH_UNIT(LENGTH_MEASURE(0.001),#12344,
'DISTANCE_ACCURACY_VALUE',
'Maximum model space distance between geometric entities at asserted c
onnectivities');
#12329=UNCERTAINTY_MEASURE_WITH_UNIT(LENGTH_MEASURE(0.001),#12344,
'DISTANCE_ACCURACY_VALUE',
'Maximum model space distance between geometric entities at asserted c
onnectivities');
#12339=(
GEOMETRIC_REPRESENTATION_CONTEXT(3)
GLOBAL_UNCERTAINTY_ASSIGNED_CONTEXT((#12325))
GLOBAL_UNIT_ASSIGNED_CONTEXT((#12344,#12346,#12347))
REPRESENTATION_CONTEXT('','3D')
);
#12343=(
GEOMETRIC_REPRESENTATION_CONTEXT(3)
GLOBAL_UNCERTAINTY_ASSIGNED_CONTEXT((#12329))
GLOBAL_UNIT_ASSIGNED_CONTEXT((#12344,#12346,#12347))
REPRESENTATION_CONTEXT('','3D')
);
#12344=(
LENGTH_UNIT()
NAMED_UNIT(*)
SI_UNIT(.CENTI.,.METRE.)
);
#12346=(
NAMED_UNIT(*)
PLANE_ANGLE_UNIT()
SI_UNIT($,.RADIAN.)
);
#12347=(
NAMED_UNIT(*)
SI_UNIT($,.STERADIAN.)
SOLID_ANGLE_UNIT()
);
#12357=SHAPE_DEFINITION_REPRESENTATION(#12370,#12404);
#12370=PRODUCT_DEFINITION_SHAPE('',$,#12418);
#12404=SHAPE_REPRESENTATION('',(#7617),#12339);
#12408=PRODUCT_DEFINITION_CONTEXT('part definition',#12449,'design');
#12418=PRODUCT_DEFINITION('Hub A','Hub A',#12431,#12408);
#12431=PRODUCT_DEFINITION_FORMATION('',$,#12460);
#12449=APPLICATION_CONTEXT(
'Core Data for Automotive Mechanical Design Process');
#12450=PRODUCT_CONTEXT('part definition',#12449,'mechanical');
#12460=PRODUCT('Hub A','Hub A','Hub A',(#12450));
#12520=COLOUR_RGB('Sky Blue',0.24,0.69,0.87);
#12521=FILL_AREA_STYLE_COLOUR('',#12520);
#12522=FILL_AREA_STYLE('',(#12521));
#12523=SURFACE_STYLE_FILL_AREA(#12522);
#12524=SURFACE_SIDE_STYLE('',(#12523));
#12525=SURFACE_STYLE_USAGE(.BOTH.,#12524);
#12526=PRESENTATION_STYLE_ASSIGNMENT((#12525));
ENDSEC;
END-ISO-10303-21;
